ISO-10303-21;
HEADER;
FILE_DESCRIPTION (('STEP AP214'),
    '1' );
FILE_NAME ('radial cylindrical roller bearing_iso_ISO 15 RCR - 3712 - 24,SI,NC,24.step',
    '2026-10-08T05:56:58',
    ( '' ),
    ( '' ),
    'SwSTEP 2.0',
    'SolidWorks 2026',
    '' );
FILE_SCHEMA (( 'AUTOMOTIVE_DESIGN' ));
ENDSEC;

DATA;
#20=EDGE_LOOP ( 'NONE', ( #15641, #11996, #7928, #5193 ) ) ;
#43=DIRECTION ( 'NONE',  ( 1.000000000000000000, 0.000000000000000000, 0.000000000000000000 ) ) ;
#48=AXIS2_PLACEMENT_3D ( 'NONE', #1489, #16900, #7577 ) ;
#79=AXIS2_PLACEMENT_3D ( 'NONE', #11870, #19566, #2860 ) ;
#86=DIRECTION ( 'NONE',  ( -0.9340060080012921873, 4.375140065418248206E-17, -0.3572572980605013271 ) ) ;
#157=ORIENTED_EDGE ( 'NONE', *, *, #10548, .F. ) ;
#171=ORIENTED_EDGE ( 'NONE', *, *, #6016, .T. ) ;
#208=CIRCLE ( 'NONE', #5304, 6.000000000000021316 ) ;
#223=VECTOR ( 'NONE', #15319, 1000.000000000000114 ) ;
#225=CARTESIAN_POINT ( 'NONE',  ( 2.500000000000002220, 0.000000000000000000, 0.000000000000000000 ) ) ;
#265=EDGE_CURVE ( 'NONE', #3536, #12799, #14477, .T. ) ;
#322=TOROIDAL_SURFACE ( 'NONE', #2538, 6.200000000000021494, 0.2000000000000003164 ) ;
#340=CARTESIAN_POINT ( 'NONE',  ( -1.869200000000000195, 0.000000000000000000, -8.239200000000002078 ) ) ;
#358=AXIS2_PLACEMENT_3D ( 'NONE', #10152, #1142, #7214 ) ;
#377=AXIS2_PLACEMENT_3D ( 'NONE', #4115, #10228, #19314 ) ;
#415=CARTESIAN_POINT ( 'NONE',  ( -1.899999999999999023, 8.279592079675421725E-16, 6.760799999999997034 ) ) ;
#458=ORIENTED_EDGE ( 'NONE', *, *, #3289, .T. ) ;
#462=AXIS2_PLACEMENT_3D ( 'NONE', #16439, #9027, #7204 ) ;
#481=LINE ( 'NONE', #7970, #4863 ) ;
#487=DIRECTION ( 'NONE',  ( 0.000000000000000000, 1.000000000000000000, -1.224646799147353207E-16 ) ) ;
#501=TOROIDAL_SURFACE ( 'NONE', #12593, 8.800000000000022027, 0.1999999999999994282 ) ;
#514=APPLICATION_CONTEXT ( 'automotive_design' ) ;
#536=CIRCLE ( 'NONE', #18400, 0.03079999999999836341 ) ;
#542=EDGE_CURVE ( 'NONE', #1723, #7592, #12575, .T. ) ;
#589=ORIENTED_EDGE ( 'NONE', *, *, #13563, .F. ) ;
#591=EDGE_CURVE ( 'NONE', #11430, #2770, #11411, .T. ) ;
#670=DIRECTION ( 'NONE',  ( 0.000000000000000000, 0.000000000000000000, -1.000000000000000000 ) ) ;
#677=VERTEX_POINT ( 'NONE', #18521 ) ;
#681=DIRECTION ( 'NONE',  ( 1.000000000000000000, -0.000000000000000000, -0.000000000000000000 ) ) ;
#686=CIRCLE ( 'NONE', #9968, 8.239200000000002078 ) ;
#696=CARTESIAN_POINT ( 'NONE',  ( -2.000000000000001776, 0.000000000000000000, -6.735000000000022524 ) ) ;
#697=DIRECTION ( 'NONE',  ( 0.000000000000000000, -1.000000000000000000, 0.000000000000000000 ) ) ;
#701=CARTESIAN_POINT ( 'NONE',  ( -2.299999999999996270, 0.000000000000000000, -6.000000000000020428 ) ) ;
#712=FACE_OUTER_BOUND ( 'NONE', #13492, .T. ) ;
#723=DIRECTION ( 'NONE',  ( 0.000000000000000000, 0.000000000000000000, -1.000000000000000000 ) ) ;
#724=AXIS2_PLACEMENT_3D ( 'NONE', #2473, #11787, #4282 ) ;
#730=DIRECTION ( 'NONE',  ( 0.000000000000000000, -1.000000000000000000, 0.000000000000000000 ) ) ;
#750=VERTEX_POINT ( 'NONE', #5499 ) ;
#759=VERTEX_POINT ( 'NONE', #16217 ) ;
#775=ORIENTED_EDGE ( 'NONE', *, *, #17901, .F. ) ;
#814=CARTESIAN_POINT ( 'NONE',  ( -90.00000000000000000, 0.000000000000000000, 0.000000000000000000 ) ) ;
#832=CIRCLE ( 'NONE', #13920, 8.265000000000021885 ) ;
#845=CARTESIAN_POINT ( 'NONE',  ( -90.00000000000000000, 1.102182119232620672E-15, 9.000000000000021316 ) ) ;
#854=CARTESIAN_POINT ( 'NONE',  ( -2.500000000000002220, 0.000000000000000000, 0.000000000000000000 ) ) ;
#869=AXIS2_PLACEMENT_3D ( 'NONE', #3599, #3403, #18508 ) ;
#877=CARTESIAN_POINT ( 'NONE',  ( -2.500000000000002220, 0.000000000000000000, 0.000000000000000000 ) ) ;
#895=CARTESIAN_POINT ( 'NONE',  ( 1.899999999999999023, 0.000000000000000000, 0.000000000000000000 ) ) ;
#908=CIRCLE ( 'NONE', #3462, 6.760799999999997034 ) ;
#925=DIRECTION ( 'NONE',  ( 1.000000000000000000, -0.000000000000000000, -0.000000000000000000 ) ) ;
#934=EDGE_LOOP ( 'NONE', ( #9051, #4555 ) ) ;
#989=EDGE_CURVE ( 'NONE', #7371, #2096, #6493, .T. ) ;
#1018=TOROIDAL_SURFACE ( 'NONE', #19533, 6.760799999999997034, 0.03079999999999868954 ) ;
#1020=AXIS2_PLACEMENT_3D ( 'NONE', #13409, #7495, #5603 ) ;
#1060=FILL_AREA_STYLE ('',( #17574 ) ) ;
#1085=TOROIDAL_SURFACE ( 'NONE', #19621, 8.239200000000002078, 0.03079999999999868954 ) ;
#1089=FACE_OUTER_BOUND ( 'NONE', #11558, .T. ) ;
#1113=ORIENTED_EDGE ( 'NONE', *, *, #17514, .F. ) ;
#1121=DIRECTION ( 'NONE',  ( 0.000000000000000000, 0.000000000000000000, -1.000000000000000000 ) ) ;
#1122=DIRECTION ( 'NONE',  ( 0.000000000000000000, 1.224646799147367998E-16, 1.000000000000000000 ) ) ;
#1123=AXIS2_PLACEMENT_3D ( 'NONE', #10070, #11847, #2733 ) ;
#1126=DIRECTION ( 'NONE',  ( 1.000000000000000000, -0.000000000000000000, -0.000000000000000000 ) ) ;
#1132=FACE_OUTER_BOUND ( 'NONE', #17975, .T. ) ;
#1135=EDGE_LOOP ( 'NONE', ( #157, #14913, #6310, #14769 ) ) ;
#1142=DIRECTION ( 'NONE',  ( 1.000000000000000000, 0.000000000000000000, 0.000000000000000000 ) ) ;
#1169=EDGE_LOOP ( 'NONE', ( #12727, #1613 ) ) ;
#1201=EDGE_LOOP ( 'NONE', ( #15506, #1113, #10005, #6475 ) ) ;
#1231=AXIS2_PLACEMENT_3D ( 'NONE', #15069, #1363, #7441 ) ;
#1311=ADVANCED_FACE ( 'NONE', ( #2968 ), #1418, .T. ) ;
#1315=CARTESIAN_POINT ( 'NONE',  ( 2.299999999999998490, 1.077689183249673761E-15, 8.800000000000023803 ) ) ;
#1317=AXIS2_PLACEMENT_3D ( 'NONE', #17345, #9757, #12746 ) ;
#1325=EDGE_CURVE ( 'NONE', #8102, #14997, #9403, .T. ) ;
#1335=TOROIDAL_SURFACE ( 'NONE', #16348, 6.760799999999997034, 0.03079999999999879709 ) ;
#1338=CIRCLE ( 'NONE', #377, 6.735000000000022524 ) ;
#1363=DIRECTION ( 'NONE',  ( -0.000000000000000000, -1.000000000000000000, -0.000000000000000000 ) ) ;
#1378=DIRECTION ( 'NONE',  ( 1.000000000000000000, -0.000000000000000000, -0.000000000000000000 ) ) ;
#1397=EDGE_CURVE ( 'NONE', #16827, #3536, #17383, .T. ) ;
#1406=CARTESIAN_POINT ( 'NONE',  ( -90.00000000000000000, 0.000000000000000000, 0.000000000000000000 ) ) ;
#1410=FACE_OUTER_BOUND ( 'NONE', #13136, .T. ) ;
#1411=TOROIDAL_SURFACE ( 'NONE', #10087, 8.239200000000002078, 0.03079999999999868954 ) ;
#1418=TOROIDAL_SURFACE ( 'NONE', #17709, 6.760799999999997034, 0.03079999999999879709 ) ;
#1424=CARTESIAN_POINT ( 'NONE',  ( 2.299999999999996270, 0.000000000000000000, 0.000000000000000000 ) ) ;
#1430=VERTEX_POINT ( 'NONE', #4765 ) ;
#1486=ADVANCED_FACE ( 'NONE', ( #2140 ), #1085, .T. ) ;
#1489=CARTESIAN_POINT ( 'NONE',  ( 2.500000000000002220, 0.000000000000000000, 0.000000000000000000 ) ) ;
#1502=DIRECTION ( 'NONE',  ( 1.000000000000000000, 0.000000000000000000, 0.000000000000000000 ) ) ;
#1523=ADVANCED_FACE ( 'NONE', ( #1132 ), #11321, .T. ) ;
#1525=DIRECTION ( 'NONE',  ( 0.000000000000000000, 0.000000000000000000, -1.000000000000000000 ) ) ;
#1526=VERTEX_POINT ( 'NONE', #19141 ) ;
#1547=AXIS2_PLACEMENT_3D ( 'NONE', #10688, #15388, #15681 ) ;
#1585=FACE_OUTER_BOUND ( 'NONE', #18734, .T. ) ;
#1602=DIRECTION ( 'NONE',  ( 1.000000000000000000, 0.000000000000000000, 0.000000000000000000 ) ) ;
#1613=ORIENTED_EDGE ( 'NONE', *, *, #5813, .F. ) ;
#1624=ORIENTED_EDGE ( 'NONE', *, *, #12199, .F. ) ;
#1634=DIRECTION ( 'NONE',  ( 0.000000000000000000, 1.000000000000000000, -1.224646799147353207E-16 ) ) ;
#1644=LINE ( 'NONE', #14046, #6665 ) ;
#1652=CIRCLE ( 'NONE', #3245, 8.265000000000021885 ) ;
#1683=DIRECTION ( 'NONE',  ( 1.000000000000000000, -0.000000000000000000, -0.000000000000000000 ) ) ;
#1695=CIRCLE ( 'NONE', #2008, 8.073750000000021743 ) ;
#1723=VERTEX_POINT ( 'NONE', #15530 ) ;
#1730=VERTEX_POINT ( 'NONE', #14025 ) ;
#1749=ADVANCED_FACE ( 'NONE', ( #15925 ), #2683, .T. ) ;
#1752=VERTEX_POINT ( 'NONE', #12726 ) ;
#1781=CARTESIAN_POINT ( 'NONE',  ( 1.869200000000000195, 0.000000000000000000, 0.000000000000000000 ) ) ;
#1782=CARTESIAN_POINT ( 'NONE',  ( 2.299999999999998934, 7.592810154713616459E-16, 6.200000000000021494 ) ) ;
#1803=VERTEX_POINT ( 'NONE', #6800 ) ;
#1819=AXIS2_PLACEMENT_3D ( 'NONE', #11106, #3500, #6289 ) ;
#1857=CARTESIAN_POINT ( 'NONE',  ( -2.500000000000001332, 6.543750000000023270, 0.000000000000000000 ) ) ;
#1873=CIRCLE ( 'NONE', #1231, 0.03079999999999923077 ) ;
#1897=LINE ( 'NONE', #4905, #5959 ) ;
#1898=CYLINDRICAL_SURFACE ( 'NONE', #12433, 8.265000000000021885 ) ;
#1904=ADVANCED_FACE ( 'NONE', ( #19208 ), #5254, .T. ) ;
#1906=AXIS2_PLACEMENT_3D ( 'NONE', #8292, #697, #12365 ) ;
#1918=ORIENTED_EDGE ( 'NONE', *, *, #989, .F. ) ;
#1922=FACE_BOUND ( 'NONE', #11178, .T. ) ;
#1929=ORIENTED_EDGE ( 'NONE', *, *, #19038, .T. ) ;
#1947=AXIS2_PLACEMENT_3D ( 'NONE', #10506, #5686, #11900 ) ;
#1949=EDGE_CURVE ( 'NONE', #14997, #8102, #3656, .T. ) ;
#1988=DIRECTION ( 'NONE',  ( 0.000000000000000000, 0.000000000000000000, -1.000000000000000000 ) ) ;
#1995=CARTESIAN_POINT ( 'NONE',  ( -2.500000000000001776, 7.592810154713614487E-16, 6.200000000000020606 ) ) ;
#2005=ORIENTED_EDGE ( 'NONE', *, *, #7729, .T. ) ;
#2008=AXIS2_PLACEMENT_3D ( 'NONE', #3465, #6251, #18667 ) ;
#2037=DIRECTION ( 'NONE',  ( -0.000000000000000000, -1.000000000000000000, -0.000000000000000000 ) ) ;
#2056=AXIS2_PLACEMENT_3D ( 'NONE', #19659, #5942, #16771 ) ;
#2074=LINE ( 'NONE', #11085, #6439 ) ;
#2096=VERTEX_POINT ( 'NONE', #3494 ) ;
#2115=VERTEX_POINT ( 'NONE', #15604 ) ;
#2119=AXIS2_PLACEMENT_3D ( 'NONE', #14323, #15924, #10119 ) ;
#2133=AXIS2_PLACEMENT_3D ( 'NONE', #1782, #487, #12397 ) ;
#2136=EDGE_CURVE ( 'NONE', #750, #9260, #17010, .T. ) ;
#2138=DIRECTION ( 'NONE',  ( 1.000000000000000000, -0.000000000000000000, -0.000000000000000000 ) ) ;
#2140=FACE_OUTER_BOUND ( 'NONE', #5350, .T. ) ;
#2155=ORIENTED_EDGE ( 'NONE', *, *, #542, .T. ) ;
#2160=DIRECTION ( 'NONE',  ( 1.000000000000000000, 0.000000000000000000, 0.000000000000000000 ) ) ;
#2188=CARTESIAN_POINT ( 'NONE',  ( -90.00000000000000000, 0.000000000000000000, 0.000000000000000000 ) ) ;
#2213=AXIS2_PLACEMENT_3D ( 'NONE', #18665, #16978, #4965 ) ;
#2241=VERTEX_POINT ( 'NONE', #696 ) ;
#2250=DIRECTION ( 'NONE',  ( 0.000000000000000000, 0.000000000000000000, -1.000000000000000000 ) ) ;
#2284=DIRECTION ( 'NONE',  ( 1.000000000000000000, 0.000000000000000000, 0.000000000000000000 ) ) ;
#2289=AXIS2_PLACEMENT_3D ( 'NONE', #6520, #8137, #11044 ) ;
#2295=EDGE_CURVE ( 'NONE', #14128, #3813, #15099, .T. ) ;
#2309=CIRCLE ( 'NONE', #724, 8.073750000000021743 ) ;
#2321=DIRECTION ( 'NONE',  ( 1.000000000000000000, 0.000000000000000000, -0.000000000000000000 ) ) ;
#2325=CARTESIAN_POINT ( 'NONE',  ( 2.299999999999998490, 0.000000000000000000, 0.000000000000000000 ) ) ;
#2326=ORIENTED_EDGE ( 'NONE', *, *, #4591, .F. ) ;
#2329=FACE_OUTER_BOUND ( 'NONE', #1169, .T. ) ;
#2331=EDGE_LOOP ( 'NONE', ( #171, #18959 ) ) ;
#2340=ORIENTED_EDGE ( 'NONE', *, *, #8723, .T. ) ;
#2353=PRODUCT_DEFINITION_SHAPE ( 'NONE', 'NONE',  #7470 ) ;
#2354=EDGE_LOOP ( 'NONE', ( #17229, #17352, #14279, #8703 ) ) ;
#2362=EDGE_CURVE ( 'NONE', #8447, #1803, #2309, .T. ) ;
#2386=DIRECTION ( 'NONE',  ( 1.000000000000000000, -0.000000000000000000, -0.000000000000000000 ) ) ;
#2397=CARTESIAN_POINT ( 'NONE',  ( -2.500000000000002220, 0.000000000000000000, -8.800000000000022027 ) ) ;
#2425=DIRECTION ( 'NONE',  ( 1.000000000000000000, -0.000000000000000000, -0.000000000000000000 ) ) ;
#2427=AXIS2_PLACEMENT_3D ( 'NONE', #2325, #8440, #13036 ) ;
#2439=CARTESIAN_POINT ( 'NONE',  ( -2.000000000000001776, 8.247996192257451316E-16, 6.735000000000022524 ) ) ;
#2473=CARTESIAN_POINT ( 'NONE',  ( -2.500000000000002220, 0.000000000000000000, 0.000000000000000000 ) ) ;
#2497=DIRECTION ( 'NONE',  ( 0.000000000000000000, 0.000000000000000000, -1.000000000000000000 ) ) ;
#2518=AXIS2_PLACEMENT_3D ( 'NONE', #340, #2037, #8030 ) ;
#2537=FACE_OUTER_BOUND ( 'NONE', #18242, .T. ) ;
#2538=AXIS2_PLACEMENT_3D ( 'NONE', #3225, #4929, #10835 ) ;
#2594=DIRECTION ( 'NONE',  ( 1.000000000000000000, -0.000000000000000000, -0.000000000000000000 ) ) ;
#2609=CIRCLE ( 'NONE', #13160, 8.265000000000021885 ) ;
#2649=ORIENTED_EDGE ( 'NONE', *, *, #14169, .F. ) ;
#2670=AXIS2_PLACEMENT_3D ( 'NONE', #5715, #2425, #11931 ) ;
#2677=DIRECTION ( 'NONE',  ( 0.000000000000000000, 0.000000000000000000, -1.000000000000000000 ) ) ;
#2683=CONICAL_SURFACE ( 'NONE', #16139, 6.735000000000022524, 0.3653297453805129935 ) ;
#2701=DIRECTION ( 'NONE',  ( 0.000000000000000000, 0.000000000000000000, -1.000000000000000000 ) ) ;
#2733=DIRECTION ( 'NONE',  ( 0.000000000000000000, 0.000000000000000000, -1.000000000000000000 ) ) ;
#2762=TOROIDAL_SURFACE ( 'NONE', #13627, 8.800000000000022027, 0.1999999999999994282 ) ;
#2763=AXIS2_PLACEMENT_3D ( 'NONE', #10589, #7963, #18482 ) ;
#2770=VERTEX_POINT ( 'NONE', #15658 ) ;
#2826=DIRECTION ( 'NONE',  ( 1.000000000000000000, 0.000000000000000000, 0.000000000000000000 ) ) ;
#2838=DIRECTION ( 'NONE',  ( 0.000000000000000000, 0.000000000000000000, -1.000000000000000000 ) ) ;
#2852=TOROIDAL_SURFACE ( 'NONE', #2213, 6.200000000000020606, 0.2000000000000005107 ) ;
#2860=DIRECTION ( 'NONE',  ( 0.000000000000000000, 0.000000000000000000, -1.000000000000000000 ) ) ;
#2862=ORIENTED_EDGE ( 'NONE', *, *, #7351, .F. ) ;
#2881=CIRCLE ( 'NONE', #14068, 0.03079999999999923077 ) ;
#2898=DIRECTION ( 'NONE',  ( 1.000000000000000000, 0.000000000000000000, 0.000000000000000000 ) ) ;
#2934=DIRECTION ( 'NONE',  ( 0.000000000000000000, 0.000000000000000000, -1.000000000000000000 ) ) ;
#2968=FACE_OUTER_BOUND ( 'NONE', #16182, .T. ) ;
#3005=ORIENTED_EDGE ( 'NONE', *, *, #2295, .F. ) ;
#3009=DIRECTION ( 'NONE',  ( 0.000000000000000000, 1.000000000000000000, -1.224646799147353207E-16 ) ) ;
#3025=FACE_OUTER_BOUND ( 'NONE', #3657, .T. ) ;
#3041=DIRECTION ( 'NONE',  ( 0.000000000000000000, 0.000000000000000000, -1.000000000000000000 ) ) ;
#3064=CARTESIAN_POINT ( 'NONE',  ( -1.869200000000000195, 0.000000000000000000, 0.000000000000000000 ) ) ;
#3086=ADVANCED_FACE ( 'NONE', ( #18218 ), #18506, .T. ) ;
#3097=VERTEX_POINT ( 'NONE', #701 ) ;
#3100=CARTESIAN_POINT ( 'NONE',  ( -90.00000000000000000, 0.000000000000000000, 0.000000000000000000 ) ) ;
#3121=ORIENTED_EDGE ( 'NONE', *, *, #16030, .T. ) ;
#3128=CARTESIAN_POINT ( 'NONE',  ( -1.886022603841227552, 0.000000000000000000, 0.000000000000000000 ) ) ;
#3136=MANIFOLD_SOLID_BREP ( 'InnerRace', #13872 ) ;
#3160=ORIENTED_EDGE ( 'NONE', *, *, #8723, .F. ) ;
#3180=VERTEX_POINT ( 'NONE', #1995 ) ;
#3184=DIRECTION ( 'NONE',  ( 1.000000000000000000, 0.000000000000000000, 0.000000000000000000 ) ) ;
#3225=CARTESIAN_POINT ( 'NONE',  ( 2.299999999999998934, 0.000000000000000000, 0.000000000000000000 ) ) ;
#3227=CARTESIAN_POINT ( 'NONE',  ( -2.000000000000001776, 1.012170579495290078E-15, 8.265000000000021885 ) ) ;
#3245=AXIS2_PLACEMENT_3D ( 'NONE', #18906, #12812, #13102 ) ;
#3273=VECTOR ( 'NONE', #9878, 1000.000000000000000 ) ;
#3275=AXIS2_PLACEMENT_3D ( 'NONE', #15712, #12907, #6784 ) ;
#3289=EDGE_CURVE ( 'NONE', #17537, #15386, #9698, .T. ) ;
#3358=DIRECTION ( 'NONE',  ( -0.000000000000000000, 0.000000000000000000, 1.000000000000000000 ) ) ;
#3369=ORIENTED_EDGE ( 'NONE', *, *, #7061, .F. ) ;
#3380=DIRECTION ( 'NONE',  ( 1.000000000000000000, -0.000000000000000000, -0.000000000000000000 ) ) ;
#3388=DIRECTION ( 'NONE',  ( 0.000000000000000000, 0.000000000000000000, -1.000000000000000000 ) ) ;
#3403=DIRECTION ( 'NONE',  ( 1.000000000000000000, 0.000000000000000000, 0.000000000000000000 ) ) ;
#3410=CIRCLE ( 'NONE', #11717, 8.800000000000023803 ) ;
#3425=EDGE_CURVE ( 'NONE', #9243, #2241, #7233, .T. ) ;
#3462=AXIS2_PLACEMENT_3D ( 'NONE', #11892, #16699, #2677 ) ;
#3465=CARTESIAN_POINT ( 'NONE',  ( -2.000000000000001776, 0.000000000000000000, 0.000000000000000000 ) ) ;
#3480=DIRECTION ( 'NONE',  ( 1.000000000000000000, 0.000000000000000000, 0.000000000000000000 ) ) ;
#3494=CARTESIAN_POINT ( 'NONE',  ( -2.000000000000001776, 0.000000000000000000, -8.073750000000021743 ) ) ;
#3500=DIRECTION ( 'NONE',  ( 1.000000000000000000, 0.000000000000000000, 0.000000000000000000 ) ) ;
#3504=CARTESIAN_POINT ( 'NONE',  ( -2.000000000000001776, 0.000000000000000000, 0.000000000000000000 ) ) ;
#3516=ORIENTED_EDGE ( 'NONE', *, *, #9638, .T. ) ;
#3521=CIRCLE ( 'NONE', #16290, 0.2000000000000005107 ) ;
#3536=VERTEX_POINT ( 'NONE', #15835 ) ;
#3549=DIRECTION ( 'NONE',  ( -1.000000000000000000, 0.000000000000000000, -0.000000000000000000 ) ) ;
#3582=DIRECTION ( 'NONE',  ( 1.000000000000000000, 0.000000000000000000, 0.000000000000000000 ) ) ;
#3590=DIRECTION ( 'NONE',  ( 1.000000000000000000, 0.000000000000000000, 0.000000000000000000 ) ) ;
#3594=FACE_OUTER_BOUND ( 'NONE', #5062, .T. ) ;
#3595=PRESENTATION_STYLE_ASSIGNMENT (( #17406 ) ) ;
#3599=CARTESIAN_POINT ( 'NONE',  ( -2.300000000000000711, 0.000000000000000000, 0.000000000000000000 ) ) ;
#3605=VERTEX_POINT ( 'NONE', #8433 ) ;
#3611=AXIS2_PLACEMENT_3D ( 'NONE', #895, #2386, #19187 ) ;
#3642=ORIENTED_EDGE ( 'NONE', *, *, #5348, .T. ) ;
#3656=CIRCLE ( 'NONE', #11652, 8.073750000000021743 ) ;
#3657=EDGE_LOOP ( 'NONE', ( #4335, #1929, #18345, #15145 ) ) ;
#3664=VECTOR ( 'NONE', #3590, 1000.000000000000000 ) ;
#3688=CIRCLE ( 'NONE', #10100, 6.543750000000017941 ) ;
#3718=EDGE_CURVE ( 'NONE', #3097, #1526, #18121, .T. ) ;
#3738=ORIENTED_EDGE ( 'NONE', *, *, #11268, .F. ) ;
#3741=DIRECTION ( 'NONE',  ( 1.000000000000000000, -0.000000000000000000, -0.000000000000000000 ) ) ;
#3767=EDGE_CURVE ( 'NONE', #2770, #6039, #18221, .T. ) ;
#3793=CARTESIAN_POINT ( 'NONE',  ( -90.00000000000000000, 9.887492094615969966E-16, 8.073750000000021743 ) ) ;
#3813=VERTEX_POINT ( 'NONE', #5091 ) ;
#3816=ADVANCED_FACE ( 'NONE', ( #11204 ), #7993, .F. ) ;
#3826=FACE_OUTER_BOUND ( 'NONE', #17914, .T. ) ;
#3829=ADVANCED_FACE ( 'NONE', ( #13912 ), #9500, .T. ) ;
#3836=DIRECTION ( 'NONE',  ( 0.000000000000000000, 0.000000000000000000, -1.000000000000000000 ) ) ;
#3871=CIRCLE ( 'NONE', #6412, 8.265000000000021885 ) ;
#3875=EDGE_CURVE ( 'NONE', #5549, #2241, #1897, .T. ) ;
#3877=CARTESIAN_POINT ( 'NONE',  ( 1.869200000000000195, 0.000000000000000000, -6.760799999999997034 ) ) ;
#3912=ORIENTED_EDGE ( 'NONE', *, *, #19038, .F. ) ;
#3923=CIRCLE ( 'NONE', #4565, 0.1999999999999987899 ) ;
#3970=ADVANCED_FACE ( 'NONE', ( #8663 ), #11968, .F. ) ;
#3972=AXIS2_PLACEMENT_3D ( 'NONE', #15953, #6160, #12279 ) ;
#4008=ORIENTED_EDGE ( 'NONE', *, *, #14952, .T. ) ;
#4052=AXIS2_PLACEMENT_3D ( 'NONE', #1406, #12008, #5593 ) ;
#4077=CARTESIAN_POINT ( 'NONE',  ( -2.000000000000001776, 0.000000000000000000, 0.000000000000000000 ) ) ;
#4080=ADVANCED_FACE ( 'NONE', ( #18858, #17261 ), #15663, .T. ) ;
#4081=DIRECTION ( 'NONE',  ( 1.000000000000000000, 0.000000000000000000, 0.000000000000000000 ) ) ;
#4115=CARTESIAN_POINT ( 'NONE',  ( 2.000000000000001776, 0.000000000000000000, 0.000000000000000000 ) ) ;
#4132=EDGE_LOOP ( 'NONE', ( #18424, #16136, #12230, #12543 ) ) ;
#4148=AXIS2_PLACEMENT_3D ( 'NONE', #11229, #18725, #15834 ) ;
#4188=DIRECTION ( 'NONE',  ( 0.000000000000000000, 0.000000000000000000, -1.000000000000000000 ) ) ;
#4194=CARTESIAN_POINT ( 'NONE',  ( -2.500000000000002220, 0.000000000000000000, -8.073750000000021743 ) ) ;
#4213=CARTESIAN_POINT ( 'NONE',  ( -90.00000000000000000, 0.000000000000000000, 0.000000000000000000 ) ) ;
#4216=ORIENTED_EDGE ( 'NONE', *, *, #14169, .T. ) ;
#4231=CARTESIAN_POINT ( 'NONE',  ( 1.899999999999999023, 0.000000000000000000, -6.760799999999997034 ) ) ;
#4241=CARTESIAN_POINT ( 'NONE',  ( -90.00000000000000000, 0.000000000000000000, -8.265000000000021885 ) ) ;
#4247=CARTESIAN_POINT ( 'NONE',  ( 2.000000000000001776, 0.000000000000000000, -6.735000000000022524 ) ) ;
#4261=EDGE_LOOP ( 'NONE', ( #10370, #6145, #6226, #4520 ) ) ;
#4282=DIRECTION ( 'NONE',  ( 0.000000000000000000, 0.000000000000000000, -1.000000000000000000 ) ) ;
#4335=ORIENTED_EDGE ( 'NONE', *, *, #12876, .F. ) ;
#4344=LINE ( 'NONE', #10160, #19320 ) ;
#4352=CARTESIAN_POINT ( 'NONE',  ( -1.869200000000000195, 1.009010990753487416E-15, 8.239200000000002078 ) ) ;
#4353=FACE_OUTER_BOUND ( 'NONE', #8058, .T. ) ;
#4405=DIRECTION ( 'NONE',  ( -1.000000000000000000, 0.000000000000000000, -0.000000000000000000 ) ) ;
#4417=AXIS2_PLACEMENT_3D ( 'NONE', #6955, #681, #16188 ) ;
#4446=CARTESIAN_POINT ( 'NONE',  ( 1.899999999999999023, 0.000000000000000000, 0.000000000000000000 ) ) ;
#4470=DIRECTION ( 'NONE',  ( 0.000000000000000000, 0.000000000000000000, -1.000000000000000000 ) ) ;
#4484=LINE ( 'NONE', #7674, #14457 ) ;
#4520=ORIENTED_EDGE ( 'NONE', *, *, #19468, .F. ) ;
#4527=DIRECTION ( 'NONE',  ( 0.000000000000000000, 0.000000000000000000, -1.000000000000000000 ) ) ;
#4534=CARTESIAN_POINT ( 'NONE',  ( 2.000000000000001776, 0.000000000000000000, -8.073750000000021743 ) ) ;
#4542=CIRCLE ( 'NONE', #17648, 9.000000000000021316 ) ;
#4555=ORIENTED_EDGE ( 'NONE', *, *, #17741, .F. ) ;
#4565=AXIS2_PLACEMENT_3D ( 'NONE', #9545, #1634, #18538 ) ;
#4577=ADVANCED_FACE ( 'NONE', ( #5512, #19218 ), #7003, .T. ) ;
#4591=EDGE_CURVE ( 'NONE', #13534, #18366, #7264, .T. ) ;
#4598=EDGE_LOOP ( 'NONE', ( #11633, #7719, #10405, #12702 ) ) ;
#4603=EDGE_CURVE ( 'NONE', #750, #1730, #18150, .T. ) ;
#4619=DIRECTION ( 'NONE',  ( 1.000000000000000000, 0.000000000000000000, 0.000000000000000000 ) ) ;
#4662=CIRCLE ( 'NONE', #8494, 6.200000000000020606 ) ;
#4677=CIRCLE ( 'NONE', #6245, 0.1999999999999987899 ) ;
#4712=FACE_OUTER_BOUND ( 'NONE', #2354, .T. ) ;
#4718=CARTESIAN_POINT ( 'NONE',  ( -90.00000000000000000, 0.000000000000000000, -8.073750000000021743 ) ) ;
#4724=FACE_OUTER_BOUND ( 'NONE', #9165, .T. ) ;
#4760=PRODUCT_DEFINITION_FORMATION_WITH_SPECIFIED_SOURCE ( 'ANY', '', #8260, .NOT_KNOWN. ) ;
#4765=CARTESIAN_POINT ( 'NONE',  ( -1.886022603841227552, 0.000000000000000000, -8.265000000000021885 ) ) ;
#4788=FACE_OUTER_BOUND ( 'NONE', #20, .T. ) ;
#4814=EDGE_CURVE ( 'NONE', #2241, #9243, #6942, .T. ) ;
#4833=CYLINDRICAL_SURFACE ( 'NONE', #17732, 8.073750000000021743 ) ;
#4863=VECTOR ( 'NONE', #17483, 1000.000000000000000 ) ;
#4872=ORIENTED_EDGE ( 'NONE', *, *, #12981, .T. ) ;
#4880=AXIS2_PLACEMENT_3D ( 'NONE', #4446, #16654, #2934 ) ;
#4900=COLOUR_RGB ( '', 0.72549020, 0.75294118, 0.79215686) ;
#4903=( NAMED_UNIT ( * ) PLANE_ANGLE_UNIT ( ) SI_UNIT ( $, .RADIAN. ) );
#4905=CARTESIAN_POINT ( 'NONE',  ( -2.000000000000001776, 0.000000000000000000, -6.735000000000022524 ) ) ;
#4906=ORIENTED_EDGE ( 'NONE', *, *, #8843, .T. ) ;
#4929=DIRECTION ( 'NONE',  ( 1.000000000000000000, 0.000000000000000000, 0.000000000000000000 ) ) ;
#4960=EDGE_CURVE ( 'NONE', #15386, #17537, #908, .T. ) ;
#4965=DIRECTION ( 'NONE',  ( 0.000000000000000000, 0.000000000000000000, -1.000000000000000000 ) ) ;
#4974=TOROIDAL_SURFACE ( 'NONE', #6867, 8.239200000000002078, 0.03079999999999868954 ) ;
#5053=EDGE_CURVE ( 'NONE', #1430, #8854, #14655, .T. ) ;
#5062=EDGE_LOOP ( 'NONE', ( #16899, #17361, #9935, #14961 ) ) ;
#5090=EDGE_CURVE ( 'NONE', #18458, #9357, #19110, .T. ) ;
#5091=CARTESIAN_POINT ( 'NONE',  ( 2.500000000000000888, 0.000000000000000000, -6.200000000000021494 ) ) ;
#5141=DIRECTION ( 'NONE',  ( 1.000000000000000000, 0.000000000000000000, 0.000000000000000000 ) ) ;
#5167=ORIENTED_EDGE ( 'NONE', *, *, #6998, .F. ) ;
#5180=AXIS2_PLACEMENT_3D ( 'NONE', #3877, #19084, #11583 ) ;
#5193=ORIENTED_EDGE ( 'NONE', *, *, #10518, .T. ) ;
#5195=DIRECTION ( 'NONE',  ( 0.000000000000000000, 0.000000000000000000, -1.000000000000000000 ) ) ;
#5254=TOROIDAL_SURFACE ( 'NONE', #16443, 8.239200000000002078, 0.03079999999999868954 ) ;
#5263=SURFACE_STYLE_USAGE ( .BOTH. , #5360 ) ;
#5286=CARTESIAN_POINT ( 'NONE',  ( 1.899999999999999023, 0.000000000000000000, 0.000000000000000000 ) ) ;
#5304=AXIS2_PLACEMENT_3D ( 'NONE', #15952, #9862, #3836 ) ;
#5324=ORIENTED_EDGE ( 'NONE', *, *, #13442, .F. ) ;
#5348=EDGE_CURVE ( 'NONE', #2770, #11430, #3688, .T. ) ;
#5350=EDGE_LOOP ( 'NONE', ( #9294, #13605, #16354, #11965 ) ) ;
#5351=CARTESIAN_POINT ( 'NONE',  ( -90.00000000000000000, 8.247996192257451316E-16, 6.735000000000022524 ) ) ;
#5360=SURFACE_SIDE_STYLE ('',( #18972 ) ) ;
#5383=DIRECTION ( 'NONE',  ( 0.9340060080012955179, 4.375140065418144668E-17, 0.3572572980604928339 ) ) ;
#5412=ORIENTED_EDGE ( 'NONE', *, *, #1397, .F. ) ;
#5428=CARTESIAN_POINT ( 'NONE',  ( 1.869199999999999973, 0.000000000000000000, 0.000000000000000000 ) ) ;
#5444=ORIENTED_EDGE ( 'NONE', *, *, #14201, .T. ) ;
#5475=DIRECTION ( 'NONE',  ( 0.000000000000000000, 0.000000000000000000, -1.000000000000000000 ) ) ;
#5477=DIRECTION ( 'NONE',  ( 1.000000000000000000, 0.000000000000000000, 0.000000000000000000 ) ) ;
#5499=CARTESIAN_POINT ( 'NONE',  ( 1.886022603841296608, 0.000000000000000000, -6.735000000000022524 ) ) ;
#5500=ORIENTED_EDGE ( 'NONE', *, *, #18232, .T. ) ;
#5512=FACE_OUTER_BOUND ( 'NONE', #7410, .T. ) ;
#5545=ORIENTED_EDGE ( 'NONE', *, *, #6637, .F. ) ;
#5549=VERTEX_POINT ( 'NONE', #13415 ) ;
#5562=EDGE_LOOP ( 'NONE', ( #14536, #9873 ) ) ;
#5593=DIRECTION ( 'NONE',  ( 0.000000000000000000, 0.000000000000000000, -1.000000000000000000 ) ) ;
#5603=DIRECTION ( 'NONE',  ( 0.000000000000000000, 0.000000000000000000, -1.000000000000000000 ) ) ;
#5605=CARTESIAN_POINT ( 'NONE',  ( 1.899999999999999245, 6.760799999999997034, 0.000000000000000000 ) ) ;
#5621=ADVANCED_FACE ( 'NONE', ( #3826 ), #19683, .T. ) ;
#5623=ORIENTED_EDGE ( 'NONE', *, *, #2362, .F. ) ;
#5636=EDGE_CURVE ( 'NONE', #17537, #1730, #536, .T. ) ;
#5638=CIRCLE ( 'NONE', #2133, 0.2000000000000005107 ) ;
#5652=ORIENTED_EDGE ( 'NONE', *, *, #7278, .F. ) ;
#5677=AXIS2_PLACEMENT_3D ( 'NONE', #5605, #2321, #5703 ) ;
#5686=DIRECTION ( 'NONE',  ( 1.000000000000000000, 0.000000000000000000, 0.000000000000000000 ) ) ;
#5690=EDGE_LOOP ( 'NONE', ( #13793, #9145, #16402, #11237 ) ) ;
#5695=EDGE_LOOP ( 'NONE', ( #7643, #9033 ) ) ;
#5696=CARTESIAN_POINT ( 'NONE',  ( -2.500000000000000888, 8.073750000000021743, 0.000000000000000000 ) ) ;
#5703=DIRECTION ( 'NONE',  ( -0.000000000000000000, 0.000000000000000000, -1.000000000000000000 ) ) ;
#5708=PLANE ( 'NONE',  #16037 ) ;
#5712=APPLICATION_CONTEXT ( 'automotive_design' ) ;
#5715=CARTESIAN_POINT ( 'NONE',  ( 1.869200000000000195, 0.000000000000000000, 0.000000000000000000 ) ) ;
#5722=CIRCLE ( 'NONE', #1906, 0.1999999999999987899 ) ;
#5733=EDGE_LOOP ( 'NONE', ( #14036, #14403, #7433, #12296 ) ) ;
#5760=ADVANCED_FACE ( 'NONE', ( #15422 ), #18726, .T. ) ;
#5773=CARTESIAN_POINT ( 'NONE',  ( 2.000000000000001776, 9.887492094615969966E-16, 8.073750000000021743 ) ) ;
#5781=EDGE_CURVE ( 'NONE', #2115, #13534, #4677, .T. ) ;
#5789=DIRECTION ( 'NONE',  ( 1.000000000000000000, 0.000000000000000000, 0.000000000000000000 ) ) ;
#5802=CARTESIAN_POINT ( 'NONE',  ( 2.000000000000001776, 0.000000000000000000, 0.000000000000000000 ) ) ;
#5808=CIRCLE ( 'NONE', #10941, 8.239200000000002078 ) ;
#5813=EDGE_CURVE ( 'NONE', #15303, #8962, #10113, .T. ) ;
#5851=CARTESIAN_POINT ( 'NONE',  ( -2.500000000000002220, 1.089935651241146723E-15, 8.800000000000022027 ) ) ;
#5865=CARTESIAN_POINT ( 'NONE',  ( 2.500000000000002220, 0.000000000000000000, 0.000000000000000000 ) ) ;
#5871=AXIS2_PLACEMENT_3D ( 'NONE', #5865, #19769, #10290 ) ;
#5893=CYLINDRICAL_SURFACE ( 'NONE', #4052, 8.265000000000021885 ) ;
#5898=DIRECTION ( 'NONE',  ( -0.000000000000000000, 0.000000000000000000, 1.000000000000000000 ) ) ;
#5939=CARTESIAN_POINT ( 'NONE',  ( -90.00000000000000000, 0.000000000000000000, 0.000000000000000000 ) ) ;
#5942=DIRECTION ( 'NONE',  ( 0.000000000000000000, 1.000000000000000000, -1.224646799147353207E-16 ) ) ;
#5959=VECTOR ( 'NONE', #17209, 1000.000000000000000 ) ;
#5976=CARTESIAN_POINT ( 'NONE',  ( -2.500000000000002220, 0.000000000000000000, 0.000000000000000000 ) ) ;
#6014=FACE_BOUND ( 'NONE', #14414, .T. ) ;
#6016=EDGE_CURVE ( 'NONE', #18366, #13534, #3410, .T. ) ;
#6022=DIRECTION ( 'NONE',  ( 1.000000000000000000, 0.000000000000000000, 0.000000000000000000 ) ) ;
#6039=VERTEX_POINT ( 'NONE', #19394 ) ;
#6084=ORIENTED_EDGE ( 'NONE', *, *, #10386, .F. ) ;
#6085=CYLINDRICAL_SURFACE ( 'NONE', #11713, 8.073750000000021743 ) ;
#6101=CARTESIAN_POINT ( 'NONE',  ( 2.299999999999998490, 0.000000000000000000, 0.000000000000000000 ) ) ;
#6145=ORIENTED_EDGE ( 'NONE', *, *, #14267, .T. ) ;
#6157=STYLED_ITEM ( 'NONE', ( #3595 ), #3136 ) ;
#6160=DIRECTION ( 'NONE',  ( 0.000000000000000000, 1.000000000000000000, -1.224646799147353207E-16 ) ) ;
#6226=ORIENTED_EDGE ( 'NONE', *, *, #16665, .T. ) ;
#6228=DIRECTION ( 'NONE',  ( 0.000000000000000000, 0.000000000000000000, -1.000000000000000000 ) ) ;
#6230=DIRECTION ( 'NONE',  ( 1.000000000000000000, 0.000000000000000000, 0.000000000000000000 ) ) ;
#6239=ORIENTED_EDGE ( 'NONE', *, *, #8236, .F. ) ;
#6240=EDGE_CURVE ( 'NONE', #14128, #1723, #5638, .T. ) ;
#6245=AXIS2_PLACEMENT_3D ( 'NONE', #1315, #3009, #7392 ) ;
#6251=DIRECTION ( 'NONE',  ( 1.000000000000000000, 0.000000000000000000, 0.000000000000000000 ) ) ;
#6280=ORIENTED_EDGE ( 'NONE', *, *, #12876, .T. ) ;
#6289=DIRECTION ( 'NONE',  ( 0.000000000000000000, 0.000000000000000000, -1.000000000000000000 ) ) ;
#6310=ORIENTED_EDGE ( 'NONE', *, *, #12373, .T. ) ;
#6342=CIRCLE ( 'NONE', #16907, 6.543750000000023270 ) ;
#6358=CARTESIAN_POINT ( 'NONE',  ( -1.899999999999999023, 0.000000000000000000, 0.000000000000000000 ) ) ;
#6387=VECTOR ( 'NONE', #5383, 1000.000000000000000 ) ;
#6402=DIRECTION ( 'NONE',  ( 0.000000000000000000, 0.000000000000000000, -1.000000000000000000 ) ) ;
#6412=AXIS2_PLACEMENT_3D ( 'NONE', #16652, #10457, #2838 ) ;
#6427=CIRCLE ( 'NONE', #11560, 8.073750000000021743 ) ;
#6432=ORIENTED_EDGE ( 'NONE', *, *, #5813, .T. ) ;
#6439=VECTOR ( 'NONE', #3480, 1000.000000000000000 ) ;
#6475=ORIENTED_EDGE ( 'NONE', *, *, #1325, .T. ) ;
#6493=CIRCLE ( 'NONE', #13855, 8.073750000000021743 ) ;
#6520=CARTESIAN_POINT ( 'NONE',  ( -2.299999999999996270, 0.000000000000000000, 0.000000000000000000 ) ) ;
#6541=AXIS2_PLACEMENT_3D ( 'NONE', #6621, #8629, #8340 ) ;
#6585=ORIENTED_EDGE ( 'NONE', *, *, #15930, .T. ) ;
#6589=ORIENTED_EDGE ( 'NONE', *, *, #7061, .T. ) ;
#6610=CARTESIAN_POINT ( 'NONE',  ( 2.500000000000002220, 0.000000000000000000, -8.073750000000021743 ) ) ;
#6612=VECTOR ( 'NONE', #15315, 1000.000000000000000 ) ;
#6620=ORIENTED_EDGE ( 'NONE', *, *, #4814, .F. ) ;
#6621=CARTESIAN_POINT ( 'NONE',  ( -2.299999999999996270, 0.000000000000000000, 0.000000000000000000 ) ) ;
#6637=EDGE_CURVE ( 'NONE', #17341, #13082, #6743, .T. ) ;
#6646=ORIENTED_EDGE ( 'NONE', *, *, #8070, .F. ) ;
#6665=VECTOR ( 'NONE', #10950, 1000.000000000000000 ) ;
#6682=ORIENTED_EDGE ( 'NONE', *, *, #265, .T. ) ;
#6705=AXIS2_PLACEMENT_3D ( 'NONE', #4352, #10460, #13552 ) ;
#6740=CIRCLE ( 'NONE', #2289, 9.000000000000019540 ) ;
#6741=AXIS2_PLACEMENT_3D ( 'NONE', #5802, #12025, #1121 ) ;
#6743=CIRCLE ( 'NONE', #358, 8.800000000000022027 ) ;
#6758=CIRCLE ( 'NONE', #12852, 6.543750000000023270 ) ;
#6763=AXIS2_PLACEMENT_3D ( 'NONE', #4213, #13615, #2701 ) ;
#6771=CARTESIAN_POINT ( 'NONE',  ( -2.300000000000000711, 0.000000000000000000, 0.000000000000000000 ) ) ;
#6784=DIRECTION ( 'NONE',  ( 0.000000000000000000, 0.000000000000000000, -1.000000000000000000 ) ) ;
#6791=DIRECTION ( 'NONE',  ( 1.000000000000000000, 0.000000000000000000, 0.000000000000000000 ) ) ;
#6794=MECHANICAL_DESIGN_GEOMETRIC_PRESENTATION_REPRESENTATION('',(#6157),#17359);
#6800=CARTESIAN_POINT ( 'NONE',  ( -2.500000000000002220, 9.887492094615969966E-16, 8.073750000000021743 ) ) ;
#6867=AXIS2_PLACEMENT_3D ( 'NONE', #18247, #18053, #4527 ) ;
#6873=DIRECTION ( 'NONE',  ( 0.000000000000000000, 0.000000000000000000, -1.000000000000000000 ) ) ;
#6875=CARTESIAN_POINT ( 'NONE',  ( 1.886022603841227330, 1.012170579495290078E-15, 8.265000000000021885 ) ) ;
#6879=CARTESIAN_POINT ( 'NONE',  ( -1.886022603841296830, 0.000000000000000000, 0.000000000000000000 ) ) ;
#6908=ORIENTED_EDGE ( 'NONE', *, *, #9173, .F. ) ;
#6923=DIRECTION ( 'NONE',  ( 1.000000000000000000, 0.000000000000000000, 0.000000000000000000 ) ) ;
#6927=ORIENTED_EDGE ( 'NONE', *, *, #5636, .T. ) ;
#6942=CIRCLE ( 'NONE', #14643, 6.735000000000022524 ) ;
#6955=CARTESIAN_POINT ( 'NONE',  ( -1.899999999999999023, 0.000000000000000000, 0.000000000000000000 ) ) ;
#6958=ADVANCED_FACE ( 'NONE', ( #18030 ), #10130, .F. ) ;
#6961=ORIENTED_EDGE ( 'NONE', *, *, #6240, .F. ) ;
#6998=EDGE_CURVE ( 'NONE', #3097, #7592, #9014, .T. ) ;
#7003=PLANE ( 'NONE',  #5677 ) ;
#7017=EDGE_LOOP ( 'NONE', ( #15486, #4008, #6084, #14742 ) ) ;
#7053=ADVANCED_FACE ( 'NONE', ( #7192 ), #10330, .T. ) ;
#7056=DIRECTION ( 'NONE',  ( 0.000000000000000000, 0.000000000000000000, -1.000000000000000000 ) ) ;
#7061=EDGE_CURVE ( 'NONE', #9260, #6039, #1338, .T. ) ;
#7066=CIRCLE ( 'NONE', #48, 6.200000000000021494 ) ;
#7105=DIRECTION ( 'NONE',  ( -0.000000000000000000, 0.000000000000000000, 1.000000000000000000 ) ) ;
#7118=DIRECTION ( 'NONE',  ( 0.000000000000000000, 0.000000000000000000, -1.000000000000000000 ) ) ;
#7122=ORIENTED_EDGE ( 'NONE', *, *, #4603, .F. ) ;
#7129=DIRECTION ( 'NONE',  ( 1.000000000000000000, 0.000000000000000000, 0.000000000000000000 ) ) ;
#7131=EDGE_LOOP ( 'NONE', ( #6908, #9425, #11251, #589 ) ) ;
#7176=AXIS2_PLACEMENT_3D ( 'NONE', #4077, #10184, #8672 ) ;
#7192=FACE_OUTER_BOUND ( 'NONE', #7864, .T. ) ;
#7194=AXIS2_PLACEMENT_3D ( 'NONE', #17120, #14314, #7901 ) ;
#7204=DIRECTION ( 'NONE',  ( 0.000000000000000000, 0.000000000000000000, -1.000000000000000000 ) ) ;
#7214=DIRECTION ( 'NONE',  ( 0.000000000000000000, 0.000000000000000000, -1.000000000000000000 ) ) ;
#7218=ORIENTED_EDGE ( 'NONE', *, *, #2362, .T. ) ;
#7224=CARTESIAN_POINT ( 'NONE',  ( -1.899999999999999023, 0.000000000000000000, 0.000000000000000000 ) ) ;
#7233=CIRCLE ( 'NONE', #2763, 6.735000000000022524 ) ;
#7254=DIRECTION ( 'NONE',  ( 1.000000000000000000, -0.000000000000000000, -0.000000000000000000 ) ) ;
#7262=CARTESIAN_POINT ( 'NONE',  ( -90.00000000000000000, 0.000000000000000000, 0.000000000000000000 ) ) ;
#7264=CIRCLE ( 'NONE', #9870, 8.800000000000023803 ) ;
#7269=DIRECTION ( 'NONE',  ( 1.000000000000000000, 0.000000000000000000, 0.000000000000000000 ) ) ;
#7278=EDGE_CURVE ( 'NONE', #17341, #3605, #9992, .T. ) ;
#7306=CARTESIAN_POINT ( 'NONE',  ( -2.000000000000000888, 8.265000000000021885, 0.000000000000000000 ) ) ;
#7330=CARTESIAN_POINT ( 'NONE',  ( -2.299999999999996270, 1.102182119232620475E-15, 9.000000000000019540 ) ) ;
#7351=EDGE_CURVE ( 'NONE', #759, #13977, #14779, .T. ) ;
#7355=ORIENTED_EDGE ( 'NONE', *, *, #5636, .F. ) ;
#7371=VERTEX_POINT ( 'NONE', #9613 ) ;
#7375=CARTESIAN_POINT ( 'NONE',  ( -2.000000000000001776, 0.000000000000000000, 0.000000000000000000 ) ) ;
#7382=CARTESIAN_POINT ( 'NONE',  ( 1.886022603841227330, 0.000000000000000000, 0.000000000000000000 ) ) ;
#7392=DIRECTION ( 'NONE',  ( 0.000000000000000000, 1.224646799147353947E-16, 1.000000000000000000 ) ) ;
#7405=ORIENTED_EDGE ( 'NONE', *, *, #8803, .T. ) ;
#7410=EDGE_LOOP ( 'NONE', ( #14781, #6682 ) ) ;
#7431=AXIS2_PLACEMENT_3D ( 'NONE', #3100, #1602, #7118 ) ;
#7433=ORIENTED_EDGE ( 'NONE', *, *, #3875, .T. ) ;
#7441=DIRECTION ( 'NONE',  ( 0.000000000000000000, 0.000000000000000000, -1.000000000000000000 ) ) ;
#7460=DIRECTION ( 'NONE',  ( 0.000000000000000000, 0.000000000000000000, 1.000000000000000000 ) ) ;
#7464=VERTEX_POINT ( 'NONE', #5773 ) ;
#7470=PRODUCT_DEFINITION ( 'UNKNOWN', '', #4760, #16000 ) ;
#7474=ORIENTED_EDGE ( 'NONE', *, *, #5090, .F. ) ;
#7495=DIRECTION ( 'NONE',  ( 1.000000000000000000, 0.000000000000000000, 0.000000000000000000 ) ) ;
#7496=ADVANCED_FACE ( 'NONE', ( #11994 ), #16298, .T. ) ;
#7551=EDGE_LOOP ( 'NONE', ( #11446, #11108, #10416, #5652 ) ) ;
#7562=FACE_OUTER_BOUND ( 'NONE', #1135, .T. ) ;
#7577=DIRECTION ( 'NONE',  ( 0.000000000000000000, 0.000000000000000000, -1.000000000000000000 ) ) ;
#7592=VERTEX_POINT ( 'NONE', #16803 ) ;
#7603=DIRECTION ( 'NONE',  ( 0.000000000000000000, 0.000000000000000000, -1.000000000000000000 ) ) ;
#7610=DIRECTION ( 'NONE',  ( 1.000000000000000000, 0.000000000000000000, 0.000000000000000000 ) ) ;
#7643=ORIENTED_EDGE ( 'NONE', *, *, #17514, .T. ) ;
#7674=CARTESIAN_POINT ( 'NONE',  ( 2.500000000000002220, 8.013782491920515573E-16, -6.543750000000017941 ) ) ;
#7675=EDGE_CURVE ( 'NONE', #11508, #9467, #5808, .T. ) ;
#7710=CARTESIAN_POINT ( 'NONE',  ( 2.500000000000002220, 0.000000000000000000, 0.000000000000000000 ) ) ;
#7719=ORIENTED_EDGE ( 'NONE', *, *, #5781, .T. ) ;
#7729=EDGE_CURVE ( 'NONE', #16827, #15303, #481, .T. ) ;
#7783=EDGE_LOOP ( 'NONE', ( #13202, #5324 ) ) ;
#7806=CARTESIAN_POINT ( 'NONE',  ( -1.869200000000000195, 0.000000000000000000, 0.000000000000000000 ) ) ;
#7854=ORIENTED_EDGE ( 'NONE', *, *, #4814, .T. ) ;
#7864=EDGE_LOOP ( 'NONE', ( #2649, #16659, #3516, #13525 ) ) ;
#7877=AXIS2_PLACEMENT_3D ( 'NONE', #7710, #4619, #1525 ) ;
#7882=FACE_OUTER_BOUND ( 'NONE', #10257, .T. ) ;
#7901=DIRECTION ( 'NONE',  ( 0.000000000000000000, 0.000000000000000000, -1.000000000000000000 ) ) ;
#7908=VERTEX_POINT ( 'NONE', #4534 ) ;
#7920=DIRECTION ( 'NONE',  ( 0.000000000000000000, 0.000000000000000000, -1.000000000000000000 ) ) ;
#7928=ORIENTED_EDGE ( 'NONE', *, *, #6998, .T. ) ;
#7961=ORIENTED_EDGE ( 'NONE', *, *, #4603, .T. ) ;
#7963=DIRECTION ( 'NONE',  ( 1.000000000000000000, 0.000000000000000000, 0.000000000000000000 ) ) ;
#7970=CARTESIAN_POINT ( 'NONE',  ( -90.00000000000000000, 1.012170579495290078E-15, 8.265000000000021885 ) ) ;
#7993=CYLINDRICAL_SURFACE ( 'NONE', #1819, 8.073750000000021743 ) ;
#8000=ORIENTED_EDGE ( 'NONE', *, *, #591, .T. ) ;
#8030=DIRECTION ( 'NONE',  ( 0.000000000000000000, 0.000000000000000000, -1.000000000000000000 ) ) ;
#8054=AXIS2_PLACEMENT_3D ( 'NONE', #1424, #7610, #19519 ) ;
#8058=EDGE_LOOP ( 'NONE', ( #7854, #4216, #5444, #16406 ) ) ;
#8070=EDGE_CURVE ( 'NONE', #13082, #14863, #3923, .T. ) ;
#8102=VERTEX_POINT ( 'NONE', #6610 ) ;
#8114=PLANE ( 'NONE',  #8510 ) ;
#8116=CARTESIAN_POINT ( 'NONE',  ( -2.000000000000001776, 0.000000000000000000, 0.000000000000000000 ) ) ;
#8133=EDGE_LOOP ( 'NONE', ( #16008, #6280 ) ) ;
#8137=DIRECTION ( 'NONE',  ( 1.000000000000000000, 0.000000000000000000, 0.000000000000000000 ) ) ;
#8142=DIRECTION ( 'NONE',  ( 0.000000000000000000, 0.000000000000000000, -1.000000000000000000 ) ) ;
#8158=LINE ( 'NONE', #5351, #3273 ) ;
#8199=DIRECTION ( 'NONE',  ( 0.000000000000000000, 0.000000000000000000, -1.000000000000000000 ) ) ;
#8236=EDGE_CURVE ( 'NONE', #7464, #7908, #9662, .T. ) ;
#8258=ORIENTED_EDGE ( 'NONE', *, *, #3767, .F. ) ;
#8260=PRODUCT ( 'radial cylindrical roller bearing_iso_ISO 15 RCR - 3712 - 24,SI,NC,24', 'radial cylindrical roller bearing_iso_ISO 15 RCR - 3712 - 24,SI,NC,24', '', ( #13860 ) ) ;
#8273=CIRCLE ( 'NONE', #11784, 6.735000000000022524 ) ;
#8276=( GEOMETRIC_REPRESENTATION_CONTEXT ( 3 ) GLOBAL_UNCERTAINTY_ASSIGNED_CONTEXT ( ( #16594 ) ) GLOBAL_UNIT_ASSIGNED_CONTEXT ( ( #10079, #13168, #14375 ) ) REPRESENTATION_CONTEXT ( 'NONE', 'WORKASPACE' ) );
#8292=CARTESIAN_POINT ( 'NONE',  ( 2.299999999999998490, 0.000000000000000000, -8.800000000000023803 ) ) ;
#8321=CIRCLE ( 'NONE', #12169, 6.760799999999997034 ) ;
#8323=CARTESIAN_POINT ( 'NONE',  ( -2.300000000000000711, 0.000000000000000000, -6.200000000000020606 ) ) ;
#8340=DIRECTION ( 'NONE',  ( 0.000000000000000000, 0.000000000000000000, -1.000000000000000000 ) ) ;
#8358=ADVANCED_FACE ( 'NONE', ( #4712 ), #1335, .T. ) ;
#8389=EDGE_CURVE ( 'NONE', #8962, #15303, #1652, .T. ) ;
#8421=PLANE ( 'NONE',  #2119 ) ;
#8433=CARTESIAN_POINT ( 'NONE',  ( -2.299999999999996270, 0.000000000000000000, -9.000000000000019540 ) ) ;
#8440=DIRECTION ( 'NONE',  ( 1.000000000000000000, 0.000000000000000000, 0.000000000000000000 ) ) ;
#8447=VERTEX_POINT ( 'NONE', #4194 ) ;
#8449=LINE ( 'NONE', #845, #14584 ) ;
#8457=EDGE_CURVE ( 'NONE', #1803, #8447, #6427, .T. ) ;
#8479=CARTESIAN_POINT ( 'NONE',  ( -90.00000000000000000, 7.347880794884145374E-16, 6.000000000000021316 ) ) ;
#8491=DIRECTION ( 'NONE',  ( 1.000000000000000000, 0.000000000000000000, 0.000000000000000000 ) ) ;
#8494=AXIS2_PLACEMENT_3D ( 'NONE', #9056, #18356, #9254 ) ;
#8510=AXIS2_PLACEMENT_3D ( 'NONE', #16839, #14222, #11122 ) ;
#8517=VERTEX_POINT ( 'NONE', #8796 ) ;
#8522=CIRCLE ( 'NONE', #19694, 6.735000000000022524 ) ;
#8550=DIRECTION ( 'NONE',  ( 0.000000000000000000, 0.000000000000000000, -1.000000000000000000 ) ) ;
#8552=CIRCLE ( 'NONE', #17174, 0.2000000000000005107 ) ;
#8583=CARTESIAN_POINT ( 'NONE',  ( 2.500000000000002220, 8.130889342088982951E-16, -6.543750000000017941 ) ) ;
#8588=ADVANCED_FACE ( 'NONE', ( #1585 ), #1018, .T. ) ;
#8593=STYLED_ITEM ( 'NONE', ( #17766 ), #14973 ) ;
#8594=CARTESIAN_POINT ( 'NONE',  ( -90.00000000000000000, 0.000000000000000000, 0.000000000000000000 ) ) ;
#8604=FACE_OUTER_BOUND ( 'NONE', #19261, .T. ) ;
#8629=DIRECTION ( 'NONE',  ( 1.000000000000000000, 0.000000000000000000, 0.000000000000000000 ) ) ;
#8632=AXIS2_PLACEMENT_3D ( 'NONE', #225, #18720, #10830 ) ;
#8639=ORIENTED_EDGE ( 'NONE', *, *, #5348, .F. ) ;
#8658=SHAPE_REPRESENTATION_RELATIONSHIP ( 'NONE' , 'NONE' ,  #19604, #14973 ) ;
#8663=FACE_OUTER_BOUND ( 'NONE', #13153, .T. ) ;
#8664=EDGE_CURVE ( 'NONE', #3813, #14128, #7066, .T. ) ;
#8672=DIRECTION ( 'NONE',  ( 0.000000000000000000, 0.000000000000000000, -1.000000000000000000 ) ) ;
#8703=ORIENTED_EDGE ( 'NONE', *, *, #13139, .F. ) ;
#8723=EDGE_CURVE ( 'NONE', #11430, #9260, #4484, .T. ) ;
#8754=EDGE_CURVE ( 'NONE', #13082, #17341, #16358, .T. ) ;
#8767=VERTEX_POINT ( 'NONE', #12786 ) ;
#8796=CARTESIAN_POINT ( 'NONE',  ( -2.500000000000002220, 8.130889342088985910E-16, 6.543750000000023270 ) ) ;
#8801=CARTESIAN_POINT ( 'NONE',  ( 1.899999999999999023, 8.279592079675421725E-16, 6.760799999999997034 ) ) ;
#8803=EDGE_CURVE ( 'NONE', #7464, #14997, #2074, .T. ) ;
#8815=DIRECTION ( 'NONE',  ( 0.000000000000000000, 0.000000000000000000, -1.000000000000000000 ) ) ;
#8843=EDGE_CURVE ( 'NONE', #2115, #1752, #17650, .T. ) ;
#8854=VERTEX_POINT ( 'NONE', #10181 ) ;
#8891=AXIS2_PLACEMENT_3D ( 'NONE', #12393, #14283, #17385 ) ;
#8948=EDGE_LOOP ( 'NONE', ( #7218, #10893 ) ) ;
#8962=VERTEX_POINT ( 'NONE', #19369 ) ;
#8969=CARTESIAN_POINT ( 'NONE',  ( 2.500000000000002220, 0.000000000000000000, 0.000000000000000000 ) ) ;
#8970=ORIENTED_EDGE ( 'NONE', *, *, #1397, .T. ) ;
#9014=LINE ( 'NONE', #16426, #16997 ) ;
#9027=DIRECTION ( 'NONE',  ( 1.000000000000000000, 0.000000000000000000, 0.000000000000000000 ) ) ;
#9033=ORIENTED_EDGE ( 'NONE', *, *, #8236, .T. ) ;
#9035=AXIS2_PLACEMENT_3D ( 'NONE', #13067, #2160, #670 ) ;
#9051=ORIENTED_EDGE ( 'NONE', *, *, #7675, .F. ) ;
#9056=CARTESIAN_POINT ( 'NONE',  ( -2.500000000000002220, 0.000000000000000000, 0.000000000000000000 ) ) ;
#9132=ORIENTED_EDGE ( 'NONE', *, *, #5781, .F. ) ;
#9145=ORIENTED_EDGE ( 'NONE', *, *, #10548, .T. ) ;
#9165=EDGE_LOOP ( 'NONE', ( #17062, #2340, #6589, #8258 ) ) ;
#9173=EDGE_CURVE ( 'NONE', #1730, #6039, #8158, .T. ) ;
#9197=DIRECTION ( 'NONE',  ( 1.000000000000000000, -0.000000000000000000, -0.000000000000000000 ) ) ;
#9206=ADVANCED_FACE ( 'NONE', ( #2537 ), #9765, .T. ) ;
#9212=EDGE_LOOP ( 'NONE', ( #7961, #15977, #3369, #10141 ) ) ;
#9228=CARTESIAN_POINT ( 'NONE',  ( 2.500000000000002220, 0.000000000000000000, -8.800000000000023803 ) ) ;
#9243=VERTEX_POINT ( 'NONE', #2439 ) ;
#9254=DIRECTION ( 'NONE',  ( 0.000000000000000000, 0.000000000000000000, -1.000000000000000000 ) ) ;
#9260=VERTEX_POINT ( 'NONE', #4247 ) ;
#9294=ORIENTED_EDGE ( 'NONE', *, *, #7675, .T. ) ;
#9296=EDGE_CURVE ( 'NONE', #7908, #8102, #4344, .T. ) ;
#9327=FACE_BOUND ( 'NONE', #18704, .T. ) ;
#9340=VECTOR ( 'NONE', #4081, 1000.000000000000000 ) ;
#9357=VERTEX_POINT ( 'NONE', #13845 ) ;
#9402=DIRECTION ( 'NONE',  ( 1.000000000000000000, 0.000000000000000000, 0.000000000000000000 ) ) ;
#9403=CIRCLE ( 'NONE', #5871, 8.073750000000021743 ) ;
#9414=( NAMED_UNIT ( * ) SI_UNIT ( $, .STERADIAN. ) SOLID_ANGLE_UNIT ( ) );
#9425=ORIENTED_EDGE ( 'NONE', *, *, #11318, .T. ) ;
#9433=FACE_OUTER_BOUND ( 'NONE', #934, .T. ) ;
#9444=VECTOR ( 'NONE', #3184, 1000.000000000000000 ) ;
#9467=VERTEX_POINT ( 'NONE', #12815 ) ;
#9491=CARTESIAN_POINT ( 'NONE',  ( -1.899999999999999023, 0.000000000000000000, 0.000000000000000000 ) ) ;
#9500=TOROIDAL_SURFACE ( 'NONE', #869, 6.200000000000020606, 0.2000000000000005107 ) ;
#9502=CARTESIAN_POINT ( 'NONE',  ( 2.299999999999996270, 0.000000000000000000, 0.000000000000000000 ) ) ;
#9545=CARTESIAN_POINT ( 'NONE',  ( -2.300000000000000711, 1.077689183249673564E-15, 8.800000000000022027 ) ) ;
#9550=ADVANCED_FACE ( 'NONE', ( #712 ), #4833, .F. ) ;
#9613=CARTESIAN_POINT ( 'NONE',  ( -2.000000000000001776, 9.887492094615969966E-16, 8.073750000000021743 ) ) ;
#9638=EDGE_CURVE ( 'NONE', #2241, #759, #12300, .T. ) ;
#9662=CIRCLE ( 'NONE', #6741, 8.073750000000021743 ) ;
#9670=ORIENTED_EDGE ( 'NONE', *, *, #13563, .T. ) ;
#9698=CIRCLE ( 'NONE', #3611, 6.760799999999997034 ) ;
#9716=( LENGTH_UNIT ( ) NAMED_UNIT ( * ) SI_UNIT ( .MILLI., .METRE. ) );
#9738=DIRECTION ( 'NONE',  ( 1.000000000000000000, 0.000000000000000000, 0.000000000000000000 ) ) ;
#9757=DIRECTION ( 'NONE',  ( -1.000000000000000000, -0.000000000000000000, -0.000000000000000000 ) ) ;
#9765=TOROIDAL_SURFACE ( 'NONE', #1123, 6.200000000000021494, 0.2000000000000003164 ) ;
#9807=DIRECTION ( 'NONE',  ( 0.000000000000000000, 0.000000000000000000, -1.000000000000000000 ) ) ;
#9825=ORIENTED_EDGE ( 'NONE', *, *, #6240, .T. ) ;
#9833=DIRECTION ( 'NONE',  ( 0.000000000000000000, 0.000000000000000000, 1.000000000000000000 ) ) ;
#9837=EDGE_CURVE ( 'NONE', #677, #12799, #17438, .T. ) ;
#9862=DIRECTION ( 'NONE',  ( 1.000000000000000000, 0.000000000000000000, 0.000000000000000000 ) ) ;
#9870=AXIS2_PLACEMENT_3D ( 'NONE', #14728, #16142, #16427 ) ;
#9873=ORIENTED_EDGE ( 'NONE', *, *, #3289, .F. ) ;
#9878=DIRECTION ( 'NONE',  ( 1.000000000000000000, 0.000000000000000000, 0.000000000000000000 ) ) ;
#9887=( NAMED_UNIT ( * ) PLANE_ANGLE_UNIT ( ) SI_UNIT ( $, .RADIAN. ) );
#9891=LINE ( 'NONE', #8479, #18161 ) ;
#9911=LINE ( 'NONE', #12901, #6387 ) ;
#9915=DIRECTION ( 'NONE',  ( 1.000000000000000000, 0.000000000000000000, 0.000000000000000000 ) ) ;
#9923=CARTESIAN_POINT ( 'NONE',  ( 2.500000000000002220, 0.000000000000000000, 0.000000000000000000 ) ) ;
#9926=DIRECTION ( 'NONE',  ( 0.000000000000000000, 0.000000000000000000, -1.000000000000000000 ) ) ;
#9935=ORIENTED_EDGE ( 'NONE', *, *, #12199, .T. ) ;
#9938=DIRECTION ( 'NONE',  ( 1.000000000000000000, 0.000000000000000000, 0.000000000000000000 ) ) ;
#9952=CARTESIAN_POINT ( 'NONE',  ( 1.999999999999999112, 8.073750000000021743, 0.000000000000000000 ) ) ;
#9954=ADVANCED_FACE ( 'NONE', ( #19471 ), #15837, .T. ) ;
#9968=AXIS2_PLACEMENT_3D ( 'NONE', #7224, #11294, #14501 ) ;
#9992=CIRCLE ( 'NONE', #3275, 0.1999999999999987899 ) ;
#10005=ORIENTED_EDGE ( 'NONE', *, *, #9296, .T. ) ;
#10070=CARTESIAN_POINT ( 'NONE',  ( 2.299999999999998934, 0.000000000000000000, 0.000000000000000000 ) ) ;
#10079=( LENGTH_UNIT ( ) NAMED_UNIT ( * ) SI_UNIT ( .MILLI., .METRE. ) );
#10087=AXIS2_PLACEMENT_3D ( 'NONE', #5428, #2138, #11352 ) ;
#10093=EDGE_CURVE ( 'NONE', #14863, #3605, #12652, .T. ) ;
#10100=AXIS2_PLACEMENT_3D ( 'NONE', #8969, #13569, #19669 ) ;
#10113=CIRCLE ( 'NONE', #7194, 8.265000000000021885 ) ;
#10119=DIRECTION ( 'NONE',  ( 0.000000000000000000, 0.000000000000000000, -1.000000000000000000 ) ) ;
#10130=CYLINDRICAL_SURFACE ( 'NONE', #1020, 6.000000000000021316 ) ;
#10141=ORIENTED_EDGE ( 'NONE', *, *, #2136, .F. ) ;
#10152=CARTESIAN_POINT ( 'NONE',  ( -2.500000000000002220, 0.000000000000000000, 0.000000000000000000 ) ) ;
#10160=CARTESIAN_POINT ( 'NONE',  ( -90.00000000000000000, 0.000000000000000000, -8.073750000000021743 ) ) ;
#10163=ADVANCED_FACE ( 'NONE', ( #19642 ), #4974, .T. ) ;
#10181=CARTESIAN_POINT ( 'NONE',  ( -1.886022603841227552, 1.012170579495290078E-15, 8.265000000000021885 ) ) ;
#10184=DIRECTION ( 'NONE',  ( 1.000000000000000000, 0.000000000000000000, 0.000000000000000000 ) ) ;
#10201=EDGE_CURVE ( 'NONE', #14216, #1430, #17949, .T. ) ;
#10228=DIRECTION ( 'NONE',  ( 1.000000000000000000, 0.000000000000000000, 0.000000000000000000 ) ) ;
#10234=EDGE_CURVE ( 'NONE', #8854, #1430, #832, .T. ) ;
#10237=FACE_BOUND ( 'NONE', #5695, .T. ) ;
#10239=VERTEX_POINT ( 'NONE', #3227 ) ;
#10247=PLANE ( 'NONE',  #12466 ) ;
#10257=EDGE_LOOP ( 'NONE', ( #6646, #16116, #15320, #10998 ) ) ;
#10290=DIRECTION ( 'NONE',  ( 0.000000000000000000, 0.000000000000000000, -1.000000000000000000 ) ) ;
#10301=DIRECTION ( 'NONE',  ( 1.000000000000000000, 0.000000000000000000, 0.000000000000000000 ) ) ;
#10330=CYLINDRICAL_SURFACE ( 'NONE', #6763, 6.735000000000022524 ) ;
#10346=EDGE_LOOP ( 'NONE', ( #5500, #8970, #3738, #14924 ) ) ;
#10350=EDGE_LOOP ( 'NONE', ( #12269, #9825, #16083, #12175 ) ) ;
#10370=ORIENTED_EDGE ( 'NONE', *, *, #14952, .F. ) ;
#10386=EDGE_CURVE ( 'NONE', #8767, #3180, #4662, .T. ) ;
#10394=ADVANCED_FACE ( 'NONE', ( #4353 ), #16564, .T. ) ;
#10405=ORIENTED_EDGE ( 'NONE', *, *, #6016, .F. ) ;
#10416=ORIENTED_EDGE ( 'NONE', *, *, #18151, .F. ) ;
#10457=DIRECTION ( 'NONE',  ( 1.000000000000000000, 0.000000000000000000, 0.000000000000000000 ) ) ;
#10460=DIRECTION ( 'NONE',  ( 0.000000000000000000, 1.000000000000000000, -1.224646799147353207E-16 ) ) ;
#10478=ORIENTED_EDGE ( 'NONE', *, *, #8664, .F. ) ;
#10506=CARTESIAN_POINT ( 'NONE',  ( 2.000000000000001776, 0.000000000000000000, 0.000000000000000000 ) ) ;
#10518=EDGE_CURVE ( 'NONE', #7592, #1723, #208, .T. ) ;
#10538=ORIENTED_EDGE ( 'NONE', *, *, #3875, .F. ) ;
#10542=DIRECTION ( 'NONE',  ( 0.000000000000000000, 0.000000000000000000, -1.000000000000000000 ) ) ;
#10548=EDGE_CURVE ( 'NONE', #14863, #2115, #8449, .T. ) ;
#10589=CARTESIAN_POINT ( 'NONE',  ( -2.000000000000001776, 0.000000000000000000, 0.000000000000000000 ) ) ;
#10592=DIRECTION ( 'NONE',  ( 0.000000000000000000, 0.000000000000000000, -1.000000000000000000 ) ) ;
#10607=CARTESIAN_POINT ( 'NONE',  ( -2.300000000000000711, 0.000000000000000000, 0.000000000000000000 ) ) ;
#10688=CARTESIAN_POINT ( 'NONE',  ( -2.000000000000001776, 0.000000000000000000, 0.000000000000000000 ) ) ;
#10767=ADVANCED_FACE ( 'NONE', ( #9327, #9433 ), #8114, .T. ) ;
#10830=DIRECTION ( 'NONE',  ( 0.000000000000000000, 0.000000000000000000, 1.000000000000000000 ) ) ;
#10833=DIRECTION ( 'NONE',  ( 0.000000000000000000, -1.000000000000000000, 0.000000000000000000 ) ) ;
#10835=DIRECTION ( 'NONE',  ( 0.000000000000000000, 0.000000000000000000, -1.000000000000000000 ) ) ;
#10841=ADVANCED_FACE ( 'NONE', ( #12921, #19114 ), #8421, .T. ) ;
#10869=FACE_OUTER_BOUND ( 'NONE', #4261, .T. ) ;
#10893=ORIENTED_EDGE ( 'NONE', *, *, #8457, .T. ) ;
#10896=CYLINDRICAL_SURFACE ( 'NONE', #14733, 6.000000000000021316 ) ;
#10941=AXIS2_PLACEMENT_3D ( 'NONE', #6358, #3380, #10592 ) ;
#10949=CIRCLE ( 'NONE', #9035, 6.200000000000020606 ) ;
#10950=DIRECTION ( 'NONE',  ( 1.000000000000000000, 0.000000000000000000, 0.000000000000000000 ) ) ;
#10955=CARTESIAN_POINT ( 'NONE',  ( 2.500000000000002220, 9.887492094615969966E-16, 8.073750000000021743 ) ) ;
#10973=ADVANCED_FACE ( 'NONE', ( #19703 ), #5893, .F. ) ;
#10998=ORIENTED_EDGE ( 'NONE', *, *, #10093, .F. ) ;
#11010=EDGE_LOOP ( 'NONE', ( #15983, #6585, #6620, #10538 ) ) ;
#11023=ADVANCED_FACE ( 'NONE', ( #17813 ), #2762, .T. ) ;
#11044=DIRECTION ( 'NONE',  ( 0.000000000000000000, 0.000000000000000000, -1.000000000000000000 ) ) ;
#11047=CARTESIAN_POINT ( 'NONE',  ( 2.500000000000000888, 7.592810154713616459E-16, 6.200000000000021494 ) ) ;
#11071=AXIS2_PLACEMENT_3D ( 'NONE', #5286, #13090, #1988 ) ;
#11085=CARTESIAN_POINT ( 'NONE',  ( -90.00000000000000000, 9.887492094615969966E-16, 8.073750000000021743 ) ) ;
#11092=ADVANCED_FACE ( 'NONE', ( #8604 ), #6085, .F. ) ;
#11106=CARTESIAN_POINT ( 'NONE',  ( -90.00000000000000000, 0.000000000000000000, 0.000000000000000000 ) ) ;
#11108=ORIENTED_EDGE ( 'NONE', *, *, #8070, .T. ) ;
#11122=DIRECTION ( 'NONE',  ( 0.000000000000000000, 0.000000000000000000, 1.000000000000000000 ) ) ;
#11133=FACE_OUTER_BOUND ( 'NONE', #2331, .T. ) ;
#11161=ORIENTED_EDGE ( 'NONE', *, *, #11318, .F. ) ;
#11178=EDGE_LOOP ( 'NONE', ( #13064, #17379 ) ) ;
#11201=FILL_AREA_STYLE_COLOUR ( '', #4900 ) ;
#11202=UNCERTAINTY_MEASURE_WITH_UNIT (LENGTH_MEASURE( 1.000000000000000082E-05 ), #11473, 'distance_accuracy_value', 'NONE');
#11204=FACE_OUTER_BOUND ( 'NONE', #1201, .T. ) ;
#11229=CARTESIAN_POINT ( 'NONE',  ( 2.499999999999998668, 8.800000000000023803, 0.000000000000000000 ) ) ;
#11237=ORIENTED_EDGE ( 'NONE', *, *, #12373, .F. ) ;
#11251=ORIENTED_EDGE ( 'NONE', *, *, #2136, .T. ) ;
#11257=DIRECTION ( 'NONE',  ( 0.000000000000000000, 0.000000000000000000, -1.000000000000000000 ) ) ;
#11268=EDGE_CURVE ( 'NONE', #12799, #3536, #12369, .T. ) ;
#11280=DIRECTION ( 'NONE',  ( 1.000000000000000000, 0.000000000000000000, 0.000000000000000000 ) ) ;
#11294=DIRECTION ( 'NONE',  ( 1.000000000000000000, -0.000000000000000000, -0.000000000000000000 ) ) ;
#11318=EDGE_CURVE ( 'NONE', #1730, #750, #8522, .T. ) ;
#11321=TOROIDAL_SURFACE ( 'NONE', #2670, 6.760799999999997034, 0.03079999999999868954 ) ;
#11332=ORIENTED_EDGE ( 'NONE', *, *, #542, .F. ) ;
#11352=DIRECTION ( 'NONE',  ( 0.000000000000000000, 0.000000000000000000, -1.000000000000000000 ) ) ;
#11355=CARTESIAN_POINT ( 'NONE',  ( -1.869200000000000195, 0.000000000000000000, 0.000000000000000000 ) ) ;
#11411=CIRCLE ( 'NONE', #7877, 6.543750000000017941 ) ;
#11430=VERTEX_POINT ( 'NONE', #8583 ) ;
#11446=ORIENTED_EDGE ( 'NONE', *, *, #6637, .T. ) ;
#11473=( LENGTH_UNIT ( ) NAMED_UNIT ( * ) SI_UNIT ( .MILLI., .METRE. ) );
#11499=CARTESIAN_POINT ( 'NONE',  ( -1.869200000000000195, 8.279592079675421725E-16, 6.760799999999997034 ) ) ;
#11508=VERTEX_POINT ( 'NONE', #18476 ) ;
#11523=DIRECTION ( 'NONE',  ( 0.000000000000000000, 0.000000000000000000, -1.000000000000000000 ) ) ;
#11535=DIRECTION ( 'NONE',  ( -1.000000000000000000, 0.000000000000000000, -0.000000000000000000 ) ) ;
#11558=EDGE_LOOP ( 'NONE', ( #3912, #775, #11837, #19234 ) ) ;
#11560=AXIS2_PLACEMENT_3D ( 'NONE', #5976, #7269, #19393 ) ;
#11577=AXIS2_PLACEMENT_3D ( 'NONE', #6879, #12711, #17212 ) ;
#11583=DIRECTION ( 'NONE',  ( 0.000000000000000000, 0.000000000000000000, -1.000000000000000000 ) ) ;
#11633=ORIENTED_EDGE ( 'NONE', *, *, #18860, .T. ) ;
#11652=AXIS2_PLACEMENT_3D ( 'NONE', #18021, #5789, #13704 ) ;
#11678=LINE ( 'NONE', #17786, #9340 ) ;
#11713=AXIS2_PLACEMENT_3D ( 'NONE', #18498, #12605, #13801 ) ;
#11717=AXIS2_PLACEMENT_3D ( 'NONE', #9923, #13295, #16010 ) ;
#11768=CARTESIAN_POINT ( 'NONE',  ( -90.00000000000000000, 0.000000000000000000, 0.000000000000000000 ) ) ;
#11784=AXIS2_PLACEMENT_3D ( 'NONE', #17847, #17948, #8550 ) ;
#11787=DIRECTION ( 'NONE',  ( 1.000000000000000000, 0.000000000000000000, 0.000000000000000000 ) ) ;
#11796=EDGE_LOOP ( 'NONE', ( #19121, #17403 ) ) ;
#11805=DIRECTION ( 'NONE',  ( 1.000000000000000000, 0.000000000000000000, 0.000000000000000000 ) ) ;
#11816=DIRECTION ( 'NONE',  ( 1.000000000000000000, 0.000000000000000000, 0.000000000000000000 ) ) ;
#11831=AXIS2_PLACEMENT_3D ( 'NONE', #7382, #15214, #19305 ) ;
#11837=ORIENTED_EDGE ( 'NONE', *, *, #10201, .T. ) ;
#11840=CARTESIAN_POINT ( 'NONE',  ( 2.500000000000002220, 1.089935651241147118E-15, 8.800000000000023803 ) ) ;
#11847=DIRECTION ( 'NONE',  ( 1.000000000000000000, 0.000000000000000000, 0.000000000000000000 ) ) ;
#11870=CARTESIAN_POINT ( 'NONE',  ( 2.299999999999996270, 0.000000000000000000, 0.000000000000000000 ) ) ;
#11892=CARTESIAN_POINT ( 'NONE',  ( 1.899999999999999023, 0.000000000000000000, 0.000000000000000000 ) ) ;
#11900=DIRECTION ( 'NONE',  ( 0.000000000000000000, 0.000000000000000000, -1.000000000000000000 ) ) ;
#11914=PLANE ( 'NONE',  #17502 ) ;
#11926=DIRECTION ( 'NONE',  ( 1.000000000000000000, 0.000000000000000000, 0.000000000000000000 ) ) ;
#11931=DIRECTION ( 'NONE',  ( 0.000000000000000000, 0.000000000000000000, -1.000000000000000000 ) ) ;
#11965=ORIENTED_EDGE ( 'NONE', *, *, #14059, .F. ) ;
#11968=CYLINDRICAL_SURFACE ( 'NONE', #16533, 8.073750000000021743 ) ;
#11981=EDGE_CURVE ( 'NONE', #3813, #7592, #8552, .T. ) ;
#11982=DIRECTION ( 'NONE',  ( 0.000000000000000000, 0.000000000000000000, -1.000000000000000000 ) ) ;
#11994=FACE_OUTER_BOUND ( 'NONE', #9212, .T. ) ;
#11996=ORIENTED_EDGE ( 'NONE', *, *, #3718, .F. ) ;
#12008=DIRECTION ( 'NONE',  ( 1.000000000000000000, 0.000000000000000000, 0.000000000000000000 ) ) ;
#12025=DIRECTION ( 'NONE',  ( 1.000000000000000000, 0.000000000000000000, 0.000000000000000000 ) ) ;
#12039=CARTESIAN_POINT ( 'NONE',  ( 2.000000000000001776, 1.012170579495290078E-15, 8.265000000000021885 ) ) ;
#12093=DIRECTION ( 'NONE',  ( 1.000000000000000000, 0.000000000000000000, 0.000000000000000000 ) ) ;
#12126=ORIENTED_EDGE ( 'NONE', *, *, #5090, .T. ) ;
#12137=DIRECTION ( 'NONE',  ( 1.000000000000000000, 0.000000000000000000, 0.000000000000000000 ) ) ;
#12169=AXIS2_PLACEMENT_3D ( 'NONE', #9491, #1683, #16895 ) ;
#12175=ORIENTED_EDGE ( 'NONE', *, *, #11981, .F. ) ;
#12199=EDGE_CURVE ( 'NONE', #677, #8962, #12927, .T. ) ;
#12215=CARTESIAN_POINT ( 'NONE',  ( -2.299999999999996270, 0.000000000000000000, 0.000000000000000000 ) ) ;
#12223=DIRECTION ( 'NONE',  ( 1.000000000000000000, 0.000000000000000000, 0.000000000000000000 ) ) ;
#12228=LINE ( 'NONE', #4718, #17316 ) ;
#12230=ORIENTED_EDGE ( 'NONE', *, *, #14059, .T. ) ;
#12246=ADVANCED_FACE ( 'NONE', ( #18117, #1410 ), #11914, .T. ) ;
#12257=DIRECTION ( 'NONE',  ( -1.000000000000000000, 0.000000000000000000, 0.000000000000000000 ) ) ;
#12269=ORIENTED_EDGE ( 'NONE', *, *, #8664, .T. ) ;
#12279=DIRECTION ( 'NONE',  ( 0.000000000000000000, 1.224646799147333486E-16, 1.000000000000000000 ) ) ;
#12296=ORIENTED_EDGE ( 'NONE', *, *, #3425, .F. ) ;
#12300=LINE ( 'NONE', #12595, #9444 ) ;
#12316=CARTESIAN_POINT ( 'NONE',  ( -90.00000000000000000, 0.000000000000000000, -9.000000000000021316 ) ) ;
#12365=DIRECTION ( 'NONE',  ( 0.000000000000000000, 0.000000000000000000, -1.000000000000000000 ) ) ;
#12369=CIRCLE ( 'NONE', #11071, 8.239200000000002078 ) ;
#12373=EDGE_CURVE ( 'NONE', #3605, #1752, #18697, .T. ) ;
#12393=CARTESIAN_POINT ( 'NONE',  ( -1.886022603841227552, 0.000000000000000000, 0.000000000000000000 ) ) ;
#12397=DIRECTION ( 'NONE',  ( 0.000000000000000000, 1.224646799147353207E-16, 1.000000000000000000 ) ) ;
#12420=DIRECTION ( 'NONE',  ( 1.000000000000000000, -0.000000000000000000, -0.000000000000000000 ) ) ;
#12433=AXIS2_PLACEMENT_3D ( 'NONE', #15807, #6022, #10542 ) ;
#12449=ORIENTED_EDGE ( 'NONE', *, *, #14267, .F. ) ;
#12466=AXIS2_PLACEMENT_3D ( 'NONE', #7306, #12137, #15241 ) ;
#12473=ORIENTED_EDGE ( 'NONE', *, *, #3767, .T. ) ;
#12543=ORIENTED_EDGE ( 'NONE', *, *, #5053, .T. ) ;
#12565=ADVANCED_FACE ( 'NONE', ( #3594 ), #12903, .F. ) ;
#12575=CIRCLE ( 'NONE', #8054, 6.000000000000021316 ) ;
#12593=AXIS2_PLACEMENT_3D ( 'NONE', #6771, #17399, #9807 ) ;
#12595=CARTESIAN_POINT ( 'NONE',  ( -90.00000000000000000, 0.000000000000000000, -6.735000000000022524 ) ) ;
#12605=DIRECTION ( 'NONE',  ( 1.000000000000000000, 0.000000000000000000, 0.000000000000000000 ) ) ;
#12652=CIRCLE ( 'NONE', #15206, 9.000000000000019540 ) ;
#12702=ORIENTED_EDGE ( 'NONE', *, *, #16030, .F. ) ;
#12705=SURFACE_SIDE_STYLE ('',( #18898 ) ) ;
#12711=DIRECTION ( 'NONE',  ( -1.000000000000000000, 0.000000000000000000, 0.000000000000000000 ) ) ;
#12726=CARTESIAN_POINT ( 'NONE',  ( 2.299999999999996270, 0.000000000000000000, -9.000000000000021316 ) ) ;
#12727=ORIENTED_EDGE ( 'NONE', *, *, #8389, .F. ) ;
#12732=PLANE ( 'NONE',  #4148 ) ;
#12746=DIRECTION ( 'NONE',  ( 0.000000000000000000, 0.000000000000000000, 1.000000000000000000 ) ) ;
#12762=CARTESIAN_POINT ( 'NONE',  ( -2.299999999999996270, 0.000000000000000000, 0.000000000000000000 ) ) ;
#12786=CARTESIAN_POINT ( 'NONE',  ( -2.500000000000001776, 0.000000000000000000, -6.200000000000020606 ) ) ;
#12790=DIRECTION ( 'NONE',  ( -0.000000000000000000, -1.000000000000000000, -0.000000000000000000 ) ) ;
#12799=VERTEX_POINT ( 'NONE', #18678 ) ;
#12801=FILL_AREA_STYLE ('',( #11201 ) ) ;
#12812=DIRECTION ( 'NONE',  ( 1.000000000000000000, 0.000000000000000000, 0.000000000000000000 ) ) ;
#12815=CARTESIAN_POINT ( 'NONE',  ( -1.899999999999999023, 1.010590785124388747E-15, 8.239200000000002078 ) ) ;
#12852=AXIS2_PLACEMENT_3D ( 'NONE', #14598, #8491, #7056 ) ;
#12876=EDGE_CURVE ( 'NONE', #10239, #14216, #15293, .T. ) ;
#12889=CARTESIAN_POINT ( 'NONE',  ( 1.869199999999999973, 0.000000000000000000, -8.239200000000002078 ) ) ;
#12901=CARTESIAN_POINT ( 'NONE',  ( -2.000000000000001776, 8.247996192257451316E-16, 6.735000000000022524 ) ) ;
#12903=CYLINDRICAL_SURFACE ( 'NONE', #19109, 8.265000000000021885 ) ;
#12907=DIRECTION ( 'NONE',  ( 0.000000000000000000, -1.000000000000000000, 0.000000000000000000 ) ) ;
#12921=FACE_OUTER_BOUND ( 'NONE', #15943, .T. ) ;
#12923=CARTESIAN_POINT ( 'NONE',  ( 1.869199999999999973, 0.000000000000000000, 0.000000000000000000 ) ) ;
#12927=LINE ( 'NONE', #19025, #13037 ) ;
#12981=EDGE_CURVE ( 'NONE', #1526, #1723, #9891, .T. ) ;
#13036=DIRECTION ( 'NONE',  ( 0.000000000000000000, 0.000000000000000000, -1.000000000000000000 ) ) ;
#13037=VECTOR ( 'NONE', #9938, 1000.000000000000000 ) ;
#13064=ORIENTED_EDGE ( 'NONE', *, *, #1325, .F. ) ;
#13067=CARTESIAN_POINT ( 'NONE',  ( -2.500000000000002220, 0.000000000000000000, 0.000000000000000000 ) ) ;
#13082=VERTEX_POINT ( 'NONE', #5851 ) ;
#13090=DIRECTION ( 'NONE',  ( 1.000000000000000000, -0.000000000000000000, -0.000000000000000000 ) ) ;
#13102=DIRECTION ( 'NONE',  ( 0.000000000000000000, 0.000000000000000000, -1.000000000000000000 ) ) ;
#13121=VECTOR ( 'NONE', #9915, 1000.000000000000000 ) ;
#13127=DIRECTION ( 'NONE',  ( 0.000000000000000000, 0.000000000000000000, 1.000000000000000000 ) ) ;
#13136=EDGE_LOOP ( 'NONE', ( #5545, #17675 ) ) ;
#13139=EDGE_CURVE ( 'NONE', #759, #9357, #1873, .T. ) ;
#13153=EDGE_LOOP ( 'NONE', ( #6239, #7405, #19332, #19610 ) ) ;
#13160=AXIS2_PLACEMENT_3D ( 'NONE', #14832, #1126, #13236 ) ;
#13168=( NAMED_UNIT ( * ) PLANE_ANGLE_UNIT ( ) SI_UNIT ( $, .RADIAN. ) );
#13198=DIRECTION ( 'NONE',  ( 0.000000000000000000, 1.000000000000000000, -1.224646799147353207E-16 ) ) ;
#13202=ORIENTED_EDGE ( 'NONE', *, *, #18978, .F. ) ;
#13236=DIRECTION ( 'NONE',  ( 0.000000000000000000, 0.000000000000000000, 1.000000000000000000 ) ) ;
#13262=CARTESIAN_POINT ( 'NONE',  ( -1.886022603841296830, 8.263794135966437014E-16, 6.735000000000022524 ) ) ;
#13266=( NAMED_UNIT ( * ) SI_UNIT ( $, .STERADIAN. ) SOLID_ANGLE_UNIT ( ) );
#13295=DIRECTION ( 'NONE',  ( 1.000000000000000000, 0.000000000000000000, 0.000000000000000000 ) ) ;
#13298=AXIS2_PLACEMENT_3D ( 'NONE', #6101, #12223, #18036 ) ;
#13320=ORIENTED_EDGE ( 'NONE', *, *, #19346, .T. ) ;
#13323=AXIS2_PLACEMENT_3D ( 'NONE', #12215, #2898, #8815 ) ;
#13399=ORIENTED_EDGE ( 'NONE', *, *, #8457, .F. ) ;
#13400=DIRECTION ( 'NONE',  ( 0.000000000000000000, 0.000000000000000000, -1.000000000000000000 ) ) ;
#13409=CARTESIAN_POINT ( 'NONE',  ( -90.00000000000000000, 0.000000000000000000, 0.000000000000000000 ) ) ;
#13415=CARTESIAN_POINT ( 'NONE',  ( -2.500000000000002220, 0.000000000000000000, -6.543750000000023270 ) ) ;
#13420=AXIS2_PLACEMENT_3D ( 'NONE', #7262, #12093, #16595 ) ;
#13442=EDGE_CURVE ( 'NONE', #8517, #5549, #6342, .T. ) ;
#13443=ORIENTED_EDGE ( 'NONE', *, *, #19346, .F. ) ;
#13492=EDGE_LOOP ( 'NONE', ( #13399, #18173, #15101, #17646 ) ) ;
#13525=ORIENTED_EDGE ( 'NONE', *, *, #7351, .T. ) ;
#13534=VERTEX_POINT ( 'NONE', #11840 ) ;
#13544=CIRCLE ( 'NONE', #6541, 6.000000000000020428 ) ;
#13552=DIRECTION ( 'NONE',  ( 0.000000000000000000, 1.224646799147333486E-16, 1.000000000000000000 ) ) ;
#13563=EDGE_CURVE ( 'NONE', #6039, #9260, #8273, .T. ) ;
#13568=ORIENTED_EDGE ( 'NONE', *, *, #18988, .T. ) ;
#13569=DIRECTION ( 'NONE',  ( 1.000000000000000000, 0.000000000000000000, 0.000000000000000000 ) ) ;
#13588=CYLINDRICAL_SURFACE ( 'NONE', #13420, 8.265000000000021885 ) ;
#13605=ORIENTED_EDGE ( 'NONE', *, *, #17234, .T. ) ;
#13615=DIRECTION ( 'NONE',  ( 1.000000000000000000, 0.000000000000000000, 0.000000000000000000 ) ) ;
#13627=AXIS2_PLACEMENT_3D ( 'NONE', #10607, #1502, #13400 ) ;
#13704=DIRECTION ( 'NONE',  ( 0.000000000000000000, 0.000000000000000000, -1.000000000000000000 ) ) ;
#13705=( GEOMETRIC_REPRESENTATION_CONTEXT ( 3 ) GLOBAL_UNCERTAINTY_ASSIGNED_CONTEXT ( ( #11202 ) ) GLOBAL_UNIT_ASSIGNED_CONTEXT ( ( #11473, #9887, #13266 ) ) REPRESENTATION_CONTEXT ( 'NONE', 'WORKASPACE' ) );
#13732=ADVANCED_FACE ( 'NONE', ( #3025 ), #1898, .F. ) ;
#13765=ORIENTED_EDGE ( 'NONE', *, *, #13139, .T. ) ;
#13793=ORIENTED_EDGE ( 'NONE', *, *, #18151, .T. ) ;
#13801=DIRECTION ( 'NONE',  ( 0.000000000000000000, 0.000000000000000000, -1.000000000000000000 ) ) ;
#13823=AXIS2_PLACEMENT_3D ( 'NONE', #8594, #10301, #4188 ) ;
#13845=CARTESIAN_POINT ( 'NONE',  ( -1.899999999999999023, 0.000000000000000000, -6.760799999999997034 ) ) ;
#13855=AXIS2_PLACEMENT_3D ( 'NONE', #7375, #11805, #15309 ) ;
#13857=ADVANCED_FACE ( 'NONE', ( #10869 ), #2852, .T. ) ;
#13860=PRODUCT_CONTEXT ( 'NONE', #514, 'mechanical' ) ;
#13872=CLOSED_SHELL ( 'NONE', ( #15466, #16422, #6958, #3829, #1749, #7496, #10394, #1904, #8588, #8358, #1486, #10973, #3970, #5760, #14357, #11023, #9550, #13732, #16986, #15337, #11092, #12246, #14413, #14594, #5621, #16437, #3816, #18177, #12565, #10163, #10767, #1311, #1523, #4577, #14292, #7053, #3086, #9954, #4080, #13857, #17662, #9206, #10841, #18110 ) ) ;
#13876=CIRCLE ( 'NONE', #2056, 0.2000000000000005107 ) ;
#13912=FACE_OUTER_BOUND ( 'NONE', #7017, .T. ) ;
#13920=AXIS2_PLACEMENT_3D ( 'NONE', #3128, #16947, #7920 ) ;
#13977=VERTEX_POINT ( 'NONE', #13262 ) ;
#13989=AXIS2_PLACEMENT_3D ( 'NONE', #14541, #925, #13127 ) ;
#14025=CARTESIAN_POINT ( 'NONE',  ( 1.886022603841296608, 8.263794135966437014E-16, 6.735000000000022524 ) ) ;
#14036=ORIENTED_EDGE ( 'NONE', *, *, #15930, .F. ) ;
#14046=CARTESIAN_POINT ( 'NONE',  ( -90.00000000000000000, 8.247996192257451316E-16, 6.735000000000022524 ) ) ;
#14059=EDGE_CURVE ( 'NONE', #11508, #1430, #17564, .T. ) ;
#14068=AXIS2_PLACEMENT_3D ( 'NONE', #11499, #13198, #17303 ) ;
#14073=ORIENTED_EDGE ( 'NONE', *, *, #18988, .F. ) ;
#14128=VERTEX_POINT ( 'NONE', #11047 ) ;
#14169=EDGE_CURVE ( 'NONE', #9243, #13977, #1644, .T. ) ;
#14201=EDGE_CURVE ( 'NONE', #13977, #759, #17870, .T. ) ;
#14216=VERTEX_POINT ( 'NONE', #17643 ) ;
#14222=DIRECTION ( 'NONE',  ( -1.000000000000000000, 0.000000000000000000, 0.000000000000000000 ) ) ;
#14249=CARTESIAN_POINT ( 'NONE',  ( -1.886022603841296830, 0.000000000000000000, 0.000000000000000000 ) ) ;
#14267=EDGE_CURVE ( 'NONE', #1526, #3097, #13544, .T. ) ;
#14279=ORIENTED_EDGE ( 'NONE', *, *, #17097, .F. ) ;
#14283=DIRECTION ( 'NONE',  ( -1.000000000000000000, 0.000000000000000000, 0.000000000000000000 ) ) ;
#14285=DIRECTION ( 'NONE',  ( 0.000000000000000000, 0.000000000000000000, -1.000000000000000000 ) ) ;
#14292=ADVANCED_FACE ( 'NONE', ( #17451 ), #1411, .T. ) ;
#14314=DIRECTION ( 'NONE',  ( 1.000000000000000000, 0.000000000000000000, 0.000000000000000000 ) ) ;
#14323=CARTESIAN_POINT ( 'NONE',  ( 2.499999999999999112, 6.200000000000021494, 0.000000000000000000 ) ) ;
#14357=ADVANCED_FACE ( 'NONE', ( #14933 ), #16736, .T. ) ;
#14362=DIRECTION ( 'NONE',  ( 1.000000000000000000, 0.000000000000000000, 0.000000000000000000 ) ) ;
#14375=( NAMED_UNIT ( * ) SI_UNIT ( $, .STERADIAN. ) SOLID_ANGLE_UNIT ( ) );
#14403=ORIENTED_EDGE ( 'NONE', *, *, #13442, .T. ) ;
#14413=ADVANCED_FACE ( 'NONE', ( #7882 ), #501, .T. ) ;
#14414=EDGE_LOOP ( 'NONE', ( #13443, #1918 ) ) ;
#14457=VECTOR ( 'NONE', #86, 1000.000000000000114 ) ;
#14477=CIRCLE ( 'NONE', #4880, 8.239200000000002078 ) ;
#14499=ORIENTED_EDGE ( 'NONE', *, *, #9837, .T. ) ;
#14501=DIRECTION ( 'NONE',  ( 0.000000000000000000, 0.000000000000000000, -1.000000000000000000 ) ) ;
#14536=ORIENTED_EDGE ( 'NONE', *, *, #4960, .F. ) ;
#14541=CARTESIAN_POINT ( 'NONE',  ( 1.886022603841296608, 0.000000000000000000, 0.000000000000000000 ) ) ;
#14584=VECTOR ( 'NONE', #6923, 1000.000000000000000 ) ;
#14594=ADVANCED_FACE ( 'NONE', ( #7562 ), #15084, .T. ) ;
#14598=CARTESIAN_POINT ( 'NONE',  ( -2.500000000000002220, 0.000000000000000000, 0.000000000000000000 ) ) ;
#14606=UNCERTAINTY_MEASURE_WITH_UNIT (LENGTH_MEASURE( 1.000000000000000082E-05 ), #9716, 'distance_accuracy_value', 'NONE');
#14643=AXIS2_PLACEMENT_3D ( 'NONE', #3504, #18703, #5195 ) ;
#14655=CIRCLE ( 'NONE', #8891, 8.265000000000021885 ) ;
#14669=COLOUR_RGB ( '', 0.72549020, 0.75294118, 0.79215686) ;
#14694=CARTESIAN_POINT ( 'NONE',  ( 1.886022603841296608, 0.000000000000000000, 0.000000000000000000 ) ) ;
#14728=CARTESIAN_POINT ( 'NONE',  ( 2.500000000000002220, 0.000000000000000000, 0.000000000000000000 ) ) ;
#14733=AXIS2_PLACEMENT_3D ( 'NONE', #18589, #9402, #3388 ) ;
#14742=ORIENTED_EDGE ( 'NONE', *, *, #16665, .F. ) ;
#14768=AXIS2_PLACEMENT_3D ( 'NONE', #17692, #2284, #5475 ) ;
#14769=ORIENTED_EDGE ( 'NONE', *, *, #8843, .F. ) ;
#14779=CIRCLE ( 'NONE', #11577, 6.735000000000022524 ) ;
#14781=ORIENTED_EDGE ( 'NONE', *, *, #11268, .T. ) ;
#14829=ORIENTED_EDGE ( 'NONE', *, *, #16877, .F. ) ;
#14832=CARTESIAN_POINT ( 'NONE',  ( 1.886022603841227330, 0.000000000000000000, 0.000000000000000000 ) ) ;
#14863=VERTEX_POINT ( 'NONE', #7330 ) ;
#14873=AXIS2_PLACEMENT_3D ( 'NONE', #12889, #12790, #18986 ) ;
#14913=ORIENTED_EDGE ( 'NONE', *, *, #10093, .T. ) ;
#14924=ORIENTED_EDGE ( 'NONE', *, *, #9837, .F. ) ;
#14927=ORIENTED_EDGE ( 'NONE', *, *, #17097, .T. ) ;
#14933=FACE_OUTER_BOUND ( 'NONE', #5690, .T. ) ;
#14952=EDGE_CURVE ( 'NONE', #1526, #3180, #13876, .T. ) ;
#14961=ORIENTED_EDGE ( 'NONE', *, *, #8389, .T. ) ;
#14973=ADVANCED_BREP_SHAPE_REPRESENTATION ( '', ( #3136, #16724 ), #8276 ) ;
#14997=VERTEX_POINT ( 'NONE', #10955 ) ;
#15069=CARTESIAN_POINT ( 'NONE',  ( -1.869200000000000195, 0.000000000000000000, -6.760799999999997034 ) ) ;
#15084=CYLINDRICAL_SURFACE ( 'NONE', #17700, 9.000000000000021316 ) ;
#15099=CIRCLE ( 'NONE', #14768, 6.200000000000021494 ) ;
#15101=ORIENTED_EDGE ( 'NONE', *, *, #989, .T. ) ;
#15145=ORIENTED_EDGE ( 'NONE', *, *, #10201, .F. ) ;
#15197=DIRECTION ( 'NONE',  ( 0.000000000000000000, 0.000000000000000000, -1.000000000000000000 ) ) ;
#15206=AXIS2_PLACEMENT_3D ( 'NONE', #12762, #14362, #2250 ) ;
#15214=DIRECTION ( 'NONE',  ( 1.000000000000000000, -0.000000000000000000, -0.000000000000000000 ) ) ;
#15241=DIRECTION ( 'NONE',  ( 0.000000000000000000, 0.000000000000000000, -1.000000000000000000 ) ) ;
#15293=CIRCLE ( 'NONE', #1547, 8.265000000000021885 ) ;
#15303=VERTEX_POINT ( 'NONE', #12039 ) ;
#15309=DIRECTION ( 'NONE',  ( 0.000000000000000000, 0.000000000000000000, -1.000000000000000000 ) ) ;
#15315=DIRECTION ( 'NONE',  ( 1.000000000000000000, 0.000000000000000000, 0.000000000000000000 ) ) ;
#15319=DIRECTION ( 'NONE',  ( -0.9340060080012921873, 0.000000000000000000, 0.3572572980605013271 ) ) ;
#15320=ORIENTED_EDGE ( 'NONE', *, *, #7278, .T. ) ;
#15337=ADVANCED_FACE ( 'NONE', ( #19729, #6014 ), #10247, .T. ) ;
#15353=CIRCLE ( 'NONE', #6705, 0.03079999999999923077 ) ;
#15381=CARTESIAN_POINT ( 'NONE',  ( -90.00000000000000000, 0.000000000000000000, 0.000000000000000000 ) ) ;
#15386=VERTEX_POINT ( 'NONE', #4231 ) ;
#15388=DIRECTION ( 'NONE',  ( 1.000000000000000000, 0.000000000000000000, 0.000000000000000000 ) ) ;
#15402=DIRECTION ( 'NONE',  ( 0.000000000000000000, 0.000000000000000000, -1.000000000000000000 ) ) ;
#15422=FACE_OUTER_BOUND ( 'NONE', #4598, .T. ) ;
#15466=ADVANCED_FACE ( 'NONE', ( #4724 ), #17889, .T. ) ;
#15486=ORIENTED_EDGE ( 'NONE', *, *, #3718, .T. ) ;
#15506=ORIENTED_EDGE ( 'NONE', *, *, #8803, .F. ) ;
#15509=CARTESIAN_POINT ( 'NONE',  ( -90.00000000000000000, 0.000000000000000000, -6.735000000000022524 ) ) ;
#15530=CARTESIAN_POINT ( 'NONE',  ( 2.299999999999996270, 7.347880794884145374E-16, 6.000000000000021316 ) ) ;
#15574=AXIS2_PLACEMENT_3D ( 'NONE', #1857, #3549, #3358 ) ;
#15604=CARTESIAN_POINT ( 'NONE',  ( 2.299999999999996270, 1.102182119232620672E-15, 9.000000000000021316 ) ) ;
#15641=ORIENTED_EDGE ( 'NONE', *, *, #12981, .F. ) ;
#15658=CARTESIAN_POINT ( 'NONE',  ( 2.500000000000002220, 0.000000000000000000, 6.543750000000017941 ) ) ;
#15663=PLANE ( 'NONE',  #15574 ) ;
#15681=DIRECTION ( 'NONE',  ( 0.000000000000000000, 0.000000000000000000, -1.000000000000000000 ) ) ;
#15703=CONICAL_SURFACE ( 'NONE', #1317, 6.543750000000017941, 0.3653297453805220418 ) ;
#15712=CARTESIAN_POINT ( 'NONE',  ( -2.300000000000000711, 0.000000000000000000, -8.800000000000022027 ) ) ;
#15770=EDGE_CURVE ( 'NONE', #16827, #677, #18542, .T. ) ;
#15807=CARTESIAN_POINT ( 'NONE',  ( -90.00000000000000000, 0.000000000000000000, 0.000000000000000000 ) ) ;
#15812=ORIENTED_EDGE ( 'NONE', *, *, #15770, .F. ) ;
#15834=DIRECTION ( 'NONE',  ( 0.000000000000000000, 0.000000000000000000, -1.000000000000000000 ) ) ;
#15835=CARTESIAN_POINT ( 'NONE',  ( 1.899999999999999023, 1.010590785124388747E-15, 8.239200000000002078 ) ) ;
#15837=CONICAL_SURFACE ( 'NONE', #7176, 6.735000000000022524, 0.3653297453805129935 ) ;
#15924=DIRECTION ( 'NONE',  ( 1.000000000000000000, 0.000000000000000000, 0.000000000000000000 ) ) ;
#15925=FACE_OUTER_BOUND ( 'NONE', #11010, .T. ) ;
#15930=EDGE_CURVE ( 'NONE', #8517, #9243, #9911, .T. ) ;
#15943=EDGE_LOOP ( 'NONE', ( #3642, #8000 ) ) ;
#15952=CARTESIAN_POINT ( 'NONE',  ( 2.299999999999996270, 0.000000000000000000, 0.000000000000000000 ) ) ;
#15953=CARTESIAN_POINT ( 'NONE',  ( 1.869199999999999973, 1.009010990753487416E-15, 8.239200000000002078 ) ) ;
#15977=ORIENTED_EDGE ( 'NONE', *, *, #9173, .T. ) ;
#15983=ORIENTED_EDGE ( 'NONE', *, *, #18978, .T. ) ;
#16000=PRODUCT_DEFINITION_CONTEXT ( 'detailed design', #5712, 'design' ) ;
#16008=ORIENTED_EDGE ( 'NONE', *, *, #17901, .T. ) ;
#16010=DIRECTION ( 'NONE',  ( 0.000000000000000000, 0.000000000000000000, -1.000000000000000000 ) ) ;
#16030=EDGE_CURVE ( 'NONE', #1752, #18366, #5722, .T. ) ;
#16037=AXIS2_PLACEMENT_3D ( 'NONE', #9952, #11535, #7105 ) ;
#16083=ORIENTED_EDGE ( 'NONE', *, *, #10518, .F. ) ;
#16116=ORIENTED_EDGE ( 'NONE', *, *, #8754, .T. ) ;
#16136=ORIENTED_EDGE ( 'NONE', *, *, #17741, .T. ) ;
#16139=AXIS2_PLACEMENT_3D ( 'NONE', #8116, #9738, #723 ) ;
#16142=DIRECTION ( 'NONE',  ( 1.000000000000000000, 0.000000000000000000, 0.000000000000000000 ) ) ;
#16172=VECTOR ( 'NONE', #2826, 1000.000000000000000 ) ;
#16182=EDGE_LOOP ( 'NONE', ( #14829, #2862, #13765, #7474 ) ) ;
#16188=DIRECTION ( 'NONE',  ( 0.000000000000000000, 0.000000000000000000, -1.000000000000000000 ) ) ;
#16217=CARTESIAN_POINT ( 'NONE',  ( -1.886022603841296830, 0.000000000000000000, -6.735000000000022524 ) ) ;
#16275=DIRECTION ( 'NONE',  ( 1.000000000000000000, 0.000000000000000000, 0.000000000000000000 ) ) ;
#16290=AXIS2_PLACEMENT_3D ( 'NONE', #8323, #730, #11523 ) ;
#16298=CYLINDRICAL_SURFACE ( 'NONE', #13823, 6.735000000000022524 ) ;
#16348=AXIS2_PLACEMENT_3D ( 'NONE', #7806, #12420, #7603 ) ;
#16354=ORIENTED_EDGE ( 'NONE', *, *, #10234, .T. ) ;
#16358=CIRCLE ( 'NONE', #17963, 8.800000000000022027 ) ;
#16373=ORIENTED_EDGE ( 'NONE', *, *, #265, .F. ) ;
#16402=ORIENTED_EDGE ( 'NONE', *, *, #18860, .F. ) ;
#16406=ORIENTED_EDGE ( 'NONE', *, *, #9638, .F. ) ;
#16422=ADVANCED_FACE ( 'NONE', ( #17135 ), #322, .T. ) ;
#16426=CARTESIAN_POINT ( 'NONE',  ( -90.00000000000000000, 0.000000000000000000, -6.000000000000021316 ) ) ;
#16427=DIRECTION ( 'NONE',  ( 0.000000000000000000, 0.000000000000000000, -1.000000000000000000 ) ) ;
#16437=ADVANCED_FACE ( 'NONE', ( #11133, #1922 ), #12732, .T. ) ;
#16439=CARTESIAN_POINT ( 'NONE',  ( -90.00000000000000000, 0.000000000000000000, 0.000000000000000000 ) ) ;
#16443=AXIS2_PLACEMENT_3D ( 'NONE', #12923, #2594, #2497 ) ;
#16533=AXIS2_PLACEMENT_3D ( 'NONE', #11768, #16275, #8199 ) ;
#16564=CYLINDRICAL_SURFACE ( 'NONE', #19031, 6.735000000000022524 ) ;
#16583=MECHANICAL_DESIGN_GEOMETRIC_PRESENTATION_REPRESENTATION('',(#8593),#13705);
#16594=UNCERTAINTY_MEASURE_WITH_UNIT (LENGTH_MEASURE( 1.000000000000000082E-05 ), #10079, 'distance_accuracy_value', 'NONE');
#16595=DIRECTION ( 'NONE',  ( 0.000000000000000000, 0.000000000000000000, -1.000000000000000000 ) ) ;
#16652=CARTESIAN_POINT ( 'NONE',  ( -2.000000000000001776, 0.000000000000000000, 0.000000000000000000 ) ) ;
#16654=DIRECTION ( 'NONE',  ( 1.000000000000000000, -0.000000000000000000, -0.000000000000000000 ) ) ;
#16659=ORIENTED_EDGE ( 'NONE', *, *, #3425, .T. ) ;
#16665=EDGE_CURVE ( 'NONE', #3097, #8767, #3521, .T. ) ;
#16699=DIRECTION ( 'NONE',  ( 1.000000000000000000, -0.000000000000000000, -0.000000000000000000 ) ) ;
#16724=AXIS2_PLACEMENT_3D ( 'NONE', #17428, #9833, #6230 ) ;
#16736=CYLINDRICAL_SURFACE ( 'NONE', #462, 9.000000000000021316 ) ;
#16754=AXIS2_PLACEMENT_3D ( 'NONE', #14249, #12257, #6228 ) ;
#16771=DIRECTION ( 'NONE',  ( 0.000000000000000000, 1.224646799147353207E-16, 1.000000000000000000 ) ) ;
#16803=CARTESIAN_POINT ( 'NONE',  ( 2.299999999999996270, 0.000000000000000000, -6.000000000000021316 ) ) ;
#16826=CARTESIAN_POINT ( 'NONE',  ( 2.500000000000002220, 0.000000000000000000, 6.543750000000017941 ) ) ;
#16827=VERTEX_POINT ( 'NONE', #6875 ) ;
#16839=CARTESIAN_POINT ( 'NONE',  ( -1.900000000000000133, 8.239200000000002078, 0.000000000000000000 ) ) ;
#16846=EDGE_LOOP ( 'NONE', ( #12449, #4872, #2155, #5167 ) ) ;
#16873=EDGE_LOOP ( 'NONE', ( #3160, #8639, #12473, #9670 ) ) ;
#16877=EDGE_CURVE ( 'NONE', #13977, #18458, #2881, .T. ) ;
#16895=DIRECTION ( 'NONE',  ( 0.000000000000000000, 0.000000000000000000, -1.000000000000000000 ) ) ;
#16899=ORIENTED_EDGE ( 'NONE', *, *, #7729, .F. ) ;
#16900=DIRECTION ( 'NONE',  ( 1.000000000000000000, 0.000000000000000000, 0.000000000000000000 ) ) ;
#16907=AXIS2_PLACEMENT_3D ( 'NONE', #854, #5141, #11257 ) ;
#16910=EDGE_CURVE ( 'NONE', #1803, #7371, #17504, .T. ) ;
#16911=ORIENTED_EDGE ( 'NONE', *, *, #11981, .T. ) ;
#16947=DIRECTION ( 'NONE',  ( -1.000000000000000000, 0.000000000000000000, 0.000000000000000000 ) ) ;
#16967=ORIENTED_EDGE ( 'NONE', *, *, #15770, .T. ) ;
#16970=CIRCLE ( 'NONE', #1947, 8.073750000000021743 ) ;
#16978=DIRECTION ( 'NONE',  ( 1.000000000000000000, 0.000000000000000000, 0.000000000000000000 ) ) ;
#16986=ADVANCED_FACE ( 'NONE', ( #1089 ), #13588, .F. ) ;
#16997=VECTOR ( 'NONE', #11816, 1000.000000000000000 ) ;
#17010=LINE ( 'NONE', #15509, #3664 ) ;
#17062=ORIENTED_EDGE ( 'NONE', *, *, #591, .F. ) ;
#17097=EDGE_CURVE ( 'NONE', #9357, #18458, #8321, .T. ) ;
#17120=CARTESIAN_POINT ( 'NONE',  ( 2.000000000000001776, 0.000000000000000000, 0.000000000000000000 ) ) ;
#17135=FACE_OUTER_BOUND ( 'NONE', #10350, .T. ) ;
#17159=SHAPE_DEFINITION_REPRESENTATION ( #2353, #19604 ) ;
#17174=AXIS2_PLACEMENT_3D ( 'NONE', #18722, #10833, #6402 ) ;
#17209=DIRECTION ( 'NONE',  ( 0.9340060080012955179, 0.000000000000000000, -0.3572572980604928339 ) ) ;
#17212=DIRECTION ( 'NONE',  ( 0.000000000000000000, 0.000000000000000000, -1.000000000000000000 ) ) ;
#17229=ORIENTED_EDGE ( 'NONE', *, *, #14201, .F. ) ;
#17234=EDGE_CURVE ( 'NONE', #9467, #8854, #15353, .T. ) ;
#17242=FACE_OUTER_BOUND ( 'NONE', #16873, .T. ) ;
#17261=FACE_OUTER_BOUND ( 'NONE', #7783, .T. ) ;
#17303=DIRECTION ( 'NONE',  ( 0.000000000000000000, 1.224646799147333486E-16, 1.000000000000000000 ) ) ;
#17316=VECTOR ( 'NONE', #11926, 1000.000000000000000 ) ;
#17335=CIRCLE ( 'NONE', #5180, 0.03079999999999836341 ) ;
#17341=VERTEX_POINT ( 'NONE', #2397 ) ;
#17345=CARTESIAN_POINT ( 'NONE',  ( 2.500000000000002220, 0.000000000000000000, 0.000000000000000000 ) ) ;
#17352=ORIENTED_EDGE ( 'NONE', *, *, #16877, .T. ) ;
#17359=( GEOMETRIC_REPRESENTATION_CONTEXT ( 3 ) GLOBAL_UNCERTAINTY_ASSIGNED_CONTEXT ( ( #14606 ) ) GLOBAL_UNIT_ASSIGNED_CONTEXT ( ( #9716, #4903, #9414 ) ) REPRESENTATION_CONTEXT ( 'NONE', 'WORKASPACE' ) );
#17361=ORIENTED_EDGE ( 'NONE', *, *, #18232, .F. ) ;
#17379=ORIENTED_EDGE ( 'NONE', *, *, #1949, .F. ) ;
#17383=CIRCLE ( 'NONE', #3972, 0.03079999999999923077 ) ;
#17385=DIRECTION ( 'NONE',  ( 0.000000000000000000, 0.000000000000000000, -1.000000000000000000 ) ) ;
#17399=DIRECTION ( 'NONE',  ( 1.000000000000000000, 0.000000000000000000, 0.000000000000000000 ) ) ;
#17403=ORIENTED_EDGE ( 'NONE', *, *, #19468, .T. ) ;
#17406=SURFACE_STYLE_USAGE ( .BOTH. , #12705 ) ;
#17416=EDGE_LOOP ( 'NONE', ( #15812, #2005, #6432, #1624 ) ) ;
#17428=CARTESIAN_POINT ( 'NONE',  ( 0.000000000000000000, 0.000000000000000000, 0.000000000000000000 ) ) ;
#17438=CIRCLE ( 'NONE', #14873, 0.03079999999999923077 ) ;
#17451=FACE_OUTER_BOUND ( 'NONE', #18848, .T. ) ;
#17483=DIRECTION ( 'NONE',  ( 1.000000000000000000, 0.000000000000000000, 0.000000000000000000 ) ) ;
#17502=AXIS2_PLACEMENT_3D ( 'NONE', #5696, #4405, #5898 ) ;
#17504=LINE ( 'NONE', #3793, #13121 ) ;
#17514=EDGE_CURVE ( 'NONE', #7908, #7464, #16970, .T. ) ;
#17537=VERTEX_POINT ( 'NONE', #8801 ) ;
#17564=CIRCLE ( 'NONE', #2518, 0.03079999999999923077 ) ;
#17574=FILL_AREA_STYLE_COLOUR ( '', #14669 ) ;
#17643=CARTESIAN_POINT ( 'NONE',  ( -2.000000000000001776, 0.000000000000000000, -8.265000000000021885 ) ) ;
#17646=ORIENTED_EDGE ( 'NONE', *, *, #18328, .F. ) ;
#17648=AXIS2_PLACEMENT_3D ( 'NONE', #9502, #3582, #15402 ) ;
#17650=CIRCLE ( 'NONE', #79, 9.000000000000021316 ) ;
#17662=ADVANCED_FACE ( 'NONE', ( #4788 ), #10896, .F. ) ;
#17675=ORIENTED_EDGE ( 'NONE', *, *, #8754, .F. ) ;
#17692=CARTESIAN_POINT ( 'NONE',  ( 2.500000000000002220, 0.000000000000000000, 0.000000000000000000 ) ) ;
#17700=AXIS2_PLACEMENT_3D ( 'NONE', #15381, #18085, #11982 ) ;
#17709=AXIS2_PLACEMENT_3D ( 'NONE', #3064, #1378, #4470 ) ;
#17732=AXIS2_PLACEMENT_3D ( 'NONE', #814, #6791, #9926 ) ;
#17741=EDGE_CURVE ( 'NONE', #9467, #11508, #686, .T. ) ;
#17766=PRESENTATION_STYLE_ASSIGNMENT (( #5263 ) ) ;
#17786=CARTESIAN_POINT ( 'NONE',  ( -90.00000000000000000, 1.012170579495290078E-15, 8.265000000000021885 ) ) ;
#17813=FACE_OUTER_BOUND ( 'NONE', #7551, .T. ) ;
#17828=DIRECTION ( 'NONE',  ( 0.000000000000000000, 1.000000000000000000, -1.224646799147353207E-16 ) ) ;
#17847=CARTESIAN_POINT ( 'NONE',  ( 2.000000000000001776, 0.000000000000000000, 0.000000000000000000 ) ) ;
#17870=CIRCLE ( 'NONE', #16754, 6.735000000000022524 ) ;
#17889=CONICAL_SURFACE ( 'NONE', #8632, 6.543750000000017941, 0.3653297453805220418 ) ;
#17901=EDGE_CURVE ( 'NONE', #14216, #10239, #3871, .T. ) ;
#17914=EDGE_LOOP ( 'NONE', ( #9132, #4906, #3121, #2326 ) ) ;
#17948=DIRECTION ( 'NONE',  ( 1.000000000000000000, 0.000000000000000000, 0.000000000000000000 ) ) ;
#17949=LINE ( 'NONE', #4241, #16172 ) ;
#17963=AXIS2_PLACEMENT_3D ( 'NONE', #877, #19077, #14285 ) ;
#17975=EDGE_LOOP ( 'NONE', ( #7355, #458, #13568, #11161 ) ) ;
#18021=CARTESIAN_POINT ( 'NONE',  ( 2.500000000000002220, 0.000000000000000000, 0.000000000000000000 ) ) ;
#18030=FACE_OUTER_BOUND ( 'NONE', #16846, .T. ) ;
#18036=DIRECTION ( 'NONE',  ( 0.000000000000000000, 0.000000000000000000, -1.000000000000000000 ) ) ;
#18053=DIRECTION ( 'NONE',  ( 1.000000000000000000, -0.000000000000000000, -0.000000000000000000 ) ) ;
#18085=DIRECTION ( 'NONE',  ( 1.000000000000000000, 0.000000000000000000, 0.000000000000000000 ) ) ;
#18110=ADVANCED_FACE ( 'NONE', ( #17242 ), #15703, .T. ) ;
#18117=FACE_BOUND ( 'NONE', #8948, .T. ) ;
#18121=CIRCLE ( 'NONE', #13323, 6.000000000000020428 ) ;
#18150=CIRCLE ( 'NONE', #13989, 6.735000000000022524 ) ;
#18151=EDGE_CURVE ( 'NONE', #3605, #14863, #6740, .T. ) ;
#18161=VECTOR ( 'NONE', #11280, 1000.000000000000000 ) ;
#18173=ORIENTED_EDGE ( 'NONE', *, *, #16910, .T. ) ;
#18177=ADVANCED_FACE ( 'NONE', ( #10237, #2329 ), #5708, .T. ) ;
#18218=FACE_OUTER_BOUND ( 'NONE', #7131, .T. ) ;
#18221=LINE ( 'NONE', #16826, #223 ) ;
#18232=EDGE_CURVE ( 'NONE', #677, #16827, #2609, .T. ) ;
#18242=EDGE_LOOP ( 'NONE', ( #6961, #18504, #16911, #11332 ) ) ;
#18247=CARTESIAN_POINT ( 'NONE',  ( -1.869200000000000195, 0.000000000000000000, 0.000000000000000000 ) ) ;
#18328=EDGE_CURVE ( 'NONE', #8447, #2096, #12228, .T. ) ;
#18345=ORIENTED_EDGE ( 'NONE', *, *, #5053, .F. ) ;
#18356=DIRECTION ( 'NONE',  ( 1.000000000000000000, 0.000000000000000000, 0.000000000000000000 ) ) ;
#18366=VERTEX_POINT ( 'NONE', #9228 ) ;
#18400=AXIS2_PLACEMENT_3D ( 'NONE', #19131, #17828, #1122 ) ;
#18424=ORIENTED_EDGE ( 'NONE', *, *, #17234, .F. ) ;
#18458=VERTEX_POINT ( 'NONE', #415 ) ;
#18476=CARTESIAN_POINT ( 'NONE',  ( -1.899999999999999023, 0.000000000000000000, -8.239200000000002078 ) ) ;
#18482=DIRECTION ( 'NONE',  ( 0.000000000000000000, 0.000000000000000000, -1.000000000000000000 ) ) ;
#18498=CARTESIAN_POINT ( 'NONE',  ( -90.00000000000000000, 0.000000000000000000, 0.000000000000000000 ) ) ;
#18504=ORIENTED_EDGE ( 'NONE', *, *, #2295, .T. ) ;
#18506=CYLINDRICAL_SURFACE ( 'NONE', #7431, 6.735000000000022524 ) ;
#18508=DIRECTION ( 'NONE',  ( 0.000000000000000000, 0.000000000000000000, -1.000000000000000000 ) ) ;
#18521=CARTESIAN_POINT ( 'NONE',  ( 1.886022603841227330, 0.000000000000000000, -8.265000000000021885 ) ) ;
#18538=DIRECTION ( 'NONE',  ( 0.000000000000000000, 1.224646799147353947E-16, 1.000000000000000000 ) ) ;
#18541=ORIENTED_EDGE ( 'NONE', *, *, #16910, .F. ) ;
#18542=CIRCLE ( 'NONE', #11831, 8.265000000000021885 ) ;
#18589=CARTESIAN_POINT ( 'NONE',  ( -90.00000000000000000, 0.000000000000000000, 0.000000000000000000 ) ) ;
#18665=CARTESIAN_POINT ( 'NONE',  ( -2.300000000000000711, 0.000000000000000000, 0.000000000000000000 ) ) ;
#18667=DIRECTION ( 'NONE',  ( 0.000000000000000000, 0.000000000000000000, -1.000000000000000000 ) ) ;
#18678=CARTESIAN_POINT ( 'NONE',  ( 1.899999999999999023, 0.000000000000000000, -8.239200000000002078 ) ) ;
#18691=EDGE_LOOP ( 'NONE', ( #10478, #3005 ) ) ;
#18697=LINE ( 'NONE', #12316, #6612 ) ;
#18703=DIRECTION ( 'NONE',  ( 1.000000000000000000, 0.000000000000000000, 0.000000000000000000 ) ) ;
#18704=EDGE_LOOP ( 'NONE', ( #14927, #12126 ) ) ;
#18720=DIRECTION ( 'NONE',  ( -1.000000000000000000, -0.000000000000000000, -0.000000000000000000 ) ) ;
#18722=CARTESIAN_POINT ( 'NONE',  ( 2.299999999999998934, 0.000000000000000000, -6.200000000000021494 ) ) ;
#18725=DIRECTION ( 'NONE',  ( 1.000000000000000000, 0.000000000000000000, 0.000000000000000000 ) ) ;
#18726=TOROIDAL_SURFACE ( 'NONE', #13298, 8.800000000000023803, 0.1999999999999994282 ) ;
#18734=EDGE_LOOP ( 'NONE', ( #19211, #6927, #7122, #14073 ) ) ;
#18848=EDGE_LOOP ( 'NONE', ( #5412, #16967, #14499, #16373 ) ) ;
#18858=FACE_BOUND ( 'NONE', #11796, .T. ) ;
#18860=EDGE_CURVE ( 'NONE', #1752, #2115, #4542, .T. ) ;
#18898=SURFACE_STYLE_FILL_AREA ( #12801 ) ;
#18906=CARTESIAN_POINT ( 'NONE',  ( 2.000000000000001776, 0.000000000000000000, 0.000000000000000000 ) ) ;
#18959=ORIENTED_EDGE ( 'NONE', *, *, #4591, .T. ) ;
#18972=SURFACE_STYLE_FILL_AREA ( #1060 ) ;
#18978=EDGE_CURVE ( 'NONE', #5549, #8517, #6758, .T. ) ;
#18986=DIRECTION ( 'NONE',  ( 0.000000000000000000, 0.000000000000000000, -1.000000000000000000 ) ) ;
#18988=EDGE_CURVE ( 'NONE', #15386, #750, #17335, .T. ) ;
#19025=CARTESIAN_POINT ( 'NONE',  ( -90.00000000000000000, 0.000000000000000000, -8.265000000000021885 ) ) ;
#19031=AXIS2_PLACEMENT_3D ( 'NONE', #5939, #43, #3041 ) ;
#19038=EDGE_CURVE ( 'NONE', #10239, #8854, #11678, .T. ) ;
#19077=DIRECTION ( 'NONE',  ( 1.000000000000000000, 0.000000000000000000, 0.000000000000000000 ) ) ;
#19084=DIRECTION ( 'NONE',  ( -0.000000000000000000, -1.000000000000000000, -0.000000000000000000 ) ) ;
#19109=AXIS2_PLACEMENT_3D ( 'NONE', #2188, #5477, #6873 ) ;
#19110=CIRCLE ( 'NONE', #4417, 6.760799999999997034 ) ;
#19114=FACE_BOUND ( 'NONE', #18691, .T. ) ;
#19121=ORIENTED_EDGE ( 'NONE', *, *, #10386, .T. ) ;
#19131=CARTESIAN_POINT ( 'NONE',  ( 1.869200000000000195, 8.279592079675421725E-16, 6.760799999999997034 ) ) ;
#19141=CARTESIAN_POINT ( 'NONE',  ( -2.299999999999996270, 7.470345474798878944E-16, 6.000000000000020428 ) ) ;
#19187=DIRECTION ( 'NONE',  ( 0.000000000000000000, 0.000000000000000000, -1.000000000000000000 ) ) ;
#19208=FACE_OUTER_BOUND ( 'NONE', #10346, .T. ) ;
#19211=ORIENTED_EDGE ( 'NONE', *, *, #4960, .T. ) ;
#19218=FACE_BOUND ( 'NONE', #5562, .T. ) ;
#19224=ORIENTED_EDGE ( 'NONE', *, *, #18328, .T. ) ;
#19234=ORIENTED_EDGE ( 'NONE', *, *, #10234, .F. ) ;
#19261=EDGE_LOOP ( 'NONE', ( #18541, #5623, #19224, #13320 ) ) ;
#19305=DIRECTION ( 'NONE',  ( 0.000000000000000000, 0.000000000000000000, 1.000000000000000000 ) ) ;
#19314=DIRECTION ( 'NONE',  ( 0.000000000000000000, 0.000000000000000000, -1.000000000000000000 ) ) ;
#19320=VECTOR ( 'NONE', #7129, 1000.000000000000000 ) ;
#19332=ORIENTED_EDGE ( 'NONE', *, *, #1949, .T. ) ;
#19346=EDGE_CURVE ( 'NONE', #2096, #7371, #1695, .T. ) ;
#19369=CARTESIAN_POINT ( 'NONE',  ( 2.000000000000001776, 0.000000000000000000, -8.265000000000021885 ) ) ;
#19393=DIRECTION ( 'NONE',  ( 0.000000000000000000, 0.000000000000000000, -1.000000000000000000 ) ) ;
#19394=CARTESIAN_POINT ( 'NONE',  ( 2.000000000000001776, 8.247996192257451316E-16, 6.735000000000022524 ) ) ;
#19468=EDGE_CURVE ( 'NONE', #3180, #8767, #10949, .T. ) ;
#19471=FACE_OUTER_BOUND ( 'NONE', #5733, .T. ) ;
#19519=DIRECTION ( 'NONE',  ( 0.000000000000000000, 0.000000000000000000, -1.000000000000000000 ) ) ;
#19533=AXIS2_PLACEMENT_3D ( 'NONE', #1781, #9197, #15197 ) ;
#19566=DIRECTION ( 'NONE',  ( 1.000000000000000000, 0.000000000000000000, 0.000000000000000000 ) ) ;
#19604=SHAPE_REPRESENTATION ( 'radial cylindrical roller bearing_iso_ISO 15 RCR - 3712 - 24,SI,NC,24', ( #16724 ), #8276 ) ;
#19610=ORIENTED_EDGE ( 'NONE', *, *, #9296, .F. ) ;
#19621=AXIS2_PLACEMENT_3D ( 'NONE', #11355, #3741, #8142 ) ;
#19642=FACE_OUTER_BOUND ( 'NONE', #4132, .T. ) ;
#19659=CARTESIAN_POINT ( 'NONE',  ( -2.300000000000000711, 7.592810154713614487E-16, 6.200000000000020606 ) ) ;
#19669=DIRECTION ( 'NONE',  ( 0.000000000000000000, 0.000000000000000000, -1.000000000000000000 ) ) ;
#19683=TOROIDAL_SURFACE ( 'NONE', #2427, 8.800000000000023803, 0.1999999999999994282 ) ;
#19694=AXIS2_PLACEMENT_3D ( 'NONE', #14694, #7254, #7460 ) ;
#19703=FACE_OUTER_BOUND ( 'NONE', #17416, .T. ) ;
#19729=FACE_OUTER_BOUND ( 'NONE', #8133, .T. ) ;
#19769=DIRECTION ( 'NONE',  ( 1.000000000000000000, 0.000000000000000000, 0.000000000000000000 ) ) ;
ENDSEC;
END-ISO-10303-21;
